ISO-10303-21;
HEADER;
/* Generated by software containing ST-Developer
 * from STEP Tools, Inc. (www.steptools.com) 
 */

FILE_DESCRIPTION(
/* description */ (''),
/* implementation_level */ '2;1');

FILE_NAME(
/* name */ '12_Spindle_Nut_1-14_Slotted.step',
/* time_stamp */ '2026-10-25T01:26:34-07:00',
/* author */ (''),
/* organization */ (''),
/* preprocessor_version */ 'ST-DEVELOPER v20.2',
/* originating_system */ 'Autodesk Translation Framework v15.15.0.0',
/* authorisation */ '');

FILE_SCHEMA (('AUTOMOTIVE_DESIGN { 1 0 10303 214 3 1 1 }'));
ENDSEC;

DATA;
#10=MECHANICAL_DESIGN_GEOMETRIC_PRESENTATION_REPRESENTATION('',(#329),#71628);
#183=(
BOUNDED_CURVE()
B_SPLINE_CURVE(2,(#61982,#61983,#61984),.UNSPECIFIED.,.F.,.F.)
B_SPLINE_CURVE_WITH_KNOTS((3,3),(0.0551833308085786,0.208603356030854),
 .UNSPECIFIED.)
CURVE()
GEOMETRIC_REPRESENTATION_ITEM()
RATIONAL_B_SPLINE_CURVE((1.00066796366419,1.00140515246647,1.00107839993824))
REPRESENTATION_ITEM('')
);
#184=(
BOUNDED_CURVE()
B_SPLINE_CURVE(2,(#61988,#61989,#61990),.UNSPECIFIED.,.F.,.F.)
B_SPLINE_CURVE_WITH_KNOTS((3,3),(0.,0.0415381994417814),.UNSPECIFIED.)
CURVE()
GEOMETRIC_REPRESENTATION_ITEM()
RATIONAL_B_SPLINE_CURVE((1.,1.,1.))
REPRESENTATION_ITEM('')
);
#185=(
BOUNDED_CURVE()
B_SPLINE_CURVE(2,(#62002,#62003,#62004),.UNSPECIFIED.,.F.,.F.)
B_SPLINE_CURVE_WITH_KNOTS((3,3),(0.146737168363919,0.166814895713845),
 .UNSPECIFIED.)
CURVE()
GEOMETRIC_REPRESENTATION_ITEM()
RATIONAL_B_SPLINE_CURVE((1.00169850871231,1.00172953563108,1.00173725401054))
REPRESENTATION_ITEM('')
);
#186=(
BOUNDED_CURVE()
B_SPLINE_CURVE(2,(#62006,#62007,#62008),.UNSPECIFIED.,.F.,.F.)
B_SPLINE_CURVE_WITH_KNOTS((3,3),(0.0286170700108403,0.0762123799831723),
 .UNSPECIFIED.)
CURVE()
GEOMETRIC_REPRESENTATION_ITEM()
RATIONAL_B_SPLINE_CURVE((1.00112886559711,1.00201824869615,1.00274341056429))
REPRESENTATION_ITEM('')
);
#187=(
BOUNDED_CURVE()
B_SPLINE_CURVE(2,(#62010,#62011,#62012),.UNSPECIFIED.,.F.,.F.)
B_SPLINE_CURVE_WITH_KNOTS((3,3),(0.460004626021665,2.01415548066414),
 .UNSPECIFIED.)
CURVE()
GEOMETRIC_REPRESENTATION_ITEM()
RATIONAL_B_SPLINE_CURVE((1.06220108868579,1.14327836336947,1.06220108868485))
REPRESENTATION_ITEM('')
);
#188=(
BOUNDED_CURVE()
B_SPLINE_CURVE(2,(#62014,#62015,#62016),.UNSPECIFIED.,.F.,.F.)
B_SPLINE_CURVE_WITH_KNOTS((3,3),(0.517898922485183,0.565329042615563),
 .UNSPECIFIED.)
CURVE()
GEOMETRIC_REPRESENTATION_ITEM()
RATIONAL_B_SPLINE_CURVE((1.00287035745076,1.00210549051843,1.00117645345012))
REPRESENTATION_ITEM('')
);
#189=(
BOUNDED_CURVE()
B_SPLINE_CURVE(2,(#62018,#62019,#62020),.UNSPECIFIED.,.F.,.F.)
B_SPLINE_CURVE_WITH_KNOTS((3,3),(0.180111955302705,0.200189682652632),
 .UNSPECIFIED.)
CURVE()
GEOMETRIC_REPRESENTATION_ITEM()
RATIONAL_B_SPLINE_CURVE((1.00173725403577,1.00172953565623,1.00169850873703))
REPRESENTATION_ITEM('')
);
#190=(
BOUNDED_CURVE()
B_SPLINE_CURVE(2,(#62021,#62022,#62023),.UNSPECIFIED.,.F.,.F.)
B_SPLINE_CURVE_WITH_KNOTS((3,3),(0.135718481594952,0.289180967053373),
 .UNSPECIFIED.)
CURVE()
GEOMETRIC_REPRESENTATION_ITEM()
RATIONAL_B_SPLINE_CURVE((1.00140882606001,1.0017347183849,1.00099631962994))
REPRESENTATION_ITEM('')
);
#191=(
BOUNDED_CURVE()
B_SPLINE_CURVE(2,(#62028,#62029,#62030),.UNSPECIFIED.,.F.,.F.)
B_SPLINE_CURVE_WITH_KNOTS((3,3),(-2.1703979840528,-2.16974314947152),
 .UNSPECIFIED.)
CURVE()
GEOMETRIC_REPRESENTATION_ITEM()
RATIONAL_B_SPLINE_CURVE((1.2052492603669,1.20540347259793,1.20555757308983))
REPRESENTATION_ITEM('')
);
#192=(
BOUNDED_CURVE()
B_SPLINE_CURVE(2,(#62060,#62061,#62062),.UNSPECIFIED.,.F.,.F.)
B_SPLINE_CURVE_WITH_KNOTS((3,3),(-0.363565876377553,-0.362911041796276),
 .UNSPECIFIED.)
CURVE()
GEOMETRIC_REPRESENTATION_ITEM()
RATIONAL_B_SPLINE_CURVE((1.20555757308983,1.20540347259792,1.20524926036689))
REPRESENTATION_ITEM('')
);
#193=(
BOUNDED_CURVE()
B_SPLINE_CURVE(2,(#62082,#62083,#62084),.UNSPECIFIED.,.F.,.F.)
B_SPLINE_CURVE_WITH_KNOTS((3,3),(0.0400329798995012,0.0815711793412347),
 .UNSPECIFIED.)
CURVE()
GEOMETRIC_REPRESENTATION_ITEM()
RATIONAL_B_SPLINE_CURVE((1.,1.,1.))
REPRESENTATION_ITEM('')
);
#194=(
BOUNDED_CURVE()
B_SPLINE_CURVE(2,(#62105,#62106,#62107),.UNSPECIFIED.,.F.,.F.)
B_SPLINE_CURVE_WITH_KNOTS((3,3),(0.280206015619899,0.367357794870773),
 .UNSPECIFIED.)
CURVE()
GEOMETRIC_REPRESENTATION_ITEM()
RATIONAL_B_SPLINE_CURVE((1.0058941656769,1.00611162505668,1.0058941656769))
REPRESENTATION_ITEM('')
);
#195=(
BOUNDED_CURVE()
B_SPLINE_CURVE(2,(#62117,#62118,#62119),.UNSPECIFIED.,.F.,.F.)
B_SPLINE_CURVE_WITH_KNOTS((3,3),(0.460004626021663,2.01415548066414),
 .UNSPECIFIED.)
CURVE()
GEOMETRIC_REPRESENTATION_ITEM()
RATIONAL_B_SPLINE_CURVE((1.06220108868579,1.14327836336948,1.06220108868485))
REPRESENTATION_ITEM('')
);
#196=(
BOUNDED_CURVE()
B_SPLINE_CURVE(2,(#62126,#62127,#62128),.UNSPECIFIED.,.F.,.F.)
B_SPLINE_CURVE_WITH_KNOTS((3,3),(0.196145060700811,2.27801504598277),
 .UNSPECIFIED.)
CURVE()
GEOMETRIC_REPRESENTATION_ITEM()
RATIONAL_B_SPLINE_CURVE((1.02999692649796,1.17548252555731,1.02999692649702))
REPRESENTATION_ITEM('')
);
#197=(
BOUNDED_CURVE()
B_SPLINE_CURVE(2,(#62143,#62144,#62145),.UNSPECIFIED.,.F.,.F.)
B_SPLINE_CURVE_WITH_KNOTS((3,3),(0.0551833308085729,0.208603356030911),
 .UNSPECIFIED.)
CURVE()
GEOMETRIC_REPRESENTATION_ITEM()
RATIONAL_B_SPLINE_CURVE((1.00066796366438,1.00140515246685,1.00107839993854))
REPRESENTATION_ITEM('')
);
#198=(
BOUNDED_CURVE()
B_SPLINE_CURVE(2,(#62149,#62150,#62151),.UNSPECIFIED.,.F.,.F.)
B_SPLINE_CURVE_WITH_KNOTS((3,3),(0.,0.0415381994417707),.UNSPECIFIED.)
CURVE()
GEOMETRIC_REPRESENTATION_ITEM()
RATIONAL_B_SPLINE_CURVE((1.,1.,1.))
REPRESENTATION_ITEM('')
);
#199=(
BOUNDED_CURVE()
B_SPLINE_CURVE(2,(#62159,#62160,#62161),.UNSPECIFIED.,.F.,.F.)
B_SPLINE_CURVE_WITH_KNOTS((3,3),(0.0400329798994619,0.0815711793412169),
 .UNSPECIFIED.)
CURVE()
GEOMETRIC_REPRESENTATION_ITEM()
RATIONAL_B_SPLINE_CURVE((1.,1.,1.))
REPRESENTATION_ITEM('')
);
#200=(
BOUNDED_CURVE()
B_SPLINE_CURVE(2,(#62179,#62180,#62181),.UNSPECIFIED.,.F.,.F.)
B_SPLINE_CURVE_WITH_KNOTS((3,3),(0.146737168392566,0.16681489574343),
 .UNSPECIFIED.)
CURVE()
GEOMETRIC_REPRESENTATION_ITEM()
RATIONAL_B_SPLINE_CURVE((1.00169850874089,1.00172953566016,1.00173725403971))
REPRESENTATION_ITEM('')
);
#201=(
BOUNDED_CURVE()
B_SPLINE_CURVE(2,(#62183,#62184,#62185),.UNSPECIFIED.,.F.,.F.)
B_SPLINE_CURVE_WITH_KNOTS((3,3),(0.0286170700108407,0.0762123799831754),
 .UNSPECIFIED.)
CURVE()
GEOMETRIC_REPRESENTATION_ITEM()
RATIONAL_B_SPLINE_CURVE((1.0011288655971,1.00201824869615,1.00274341056429))
REPRESENTATION_ITEM('')
);
#202=(
BOUNDED_CURVE()
B_SPLINE_CURVE(2,(#62187,#62188,#62189),.UNSPECIFIED.,.F.,.F.)
B_SPLINE_CURVE_WITH_KNOTS((3,3),(0.460004626021664,2.01415548066414),
 .UNSPECIFIED.)
CURVE()
GEOMETRIC_REPRESENTATION_ITEM()
RATIONAL_B_SPLINE_CURVE((1.06220108868579,1.14327836336947,1.06220108868485))
REPRESENTATION_ITEM('')
);
#203=(
BOUNDED_CURVE()
B_SPLINE_CURVE(2,(#62191,#62192,#62193),.UNSPECIFIED.,.F.,.F.)
B_SPLINE_CURVE_WITH_KNOTS((3,3),(0.517898922485173,0.565329042615554),
 .UNSPECIFIED.)
CURVE()
GEOMETRIC_REPRESENTATION_ITEM()
RATIONAL_B_SPLINE_CURVE((1.00287035745075,1.00210549051842,1.00117645345012))
REPRESENTATION_ITEM('')
);
#204=(
BOUNDED_CURVE()
B_SPLINE_CURVE(2,(#62195,#62196,#62197),.UNSPECIFIED.,.F.,.F.)
B_SPLINE_CURVE_WITH_KNOTS((3,3),(0.180111955322094,0.200189682671483),
 .UNSPECIFIED.)
CURVE()
GEOMETRIC_REPRESENTATION_ITEM()
RATIONAL_B_SPLINE_CURVE((1.00173725402072,1.00172953564122,1.00169850872227))
REPRESENTATION_ITEM('')
);
#205=(
BOUNDED_CURVE()
B_SPLINE_CURVE(2,(#62198,#62199,#62200),.UNSPECIFIED.,.F.,.F.)
B_SPLINE_CURVE_WITH_KNOTS((3,3),(0.13571848159495,0.289180967053359),
 .UNSPECIFIED.)
CURVE()
GEOMETRIC_REPRESENTATION_ITEM()
RATIONAL_B_SPLINE_CURVE((1.00140882605995,1.00173471838483,1.0009963196299))
REPRESENTATION_ITEM('')
);
#206=(
BOUNDED_CURVE()
B_SPLINE_CURVE(2,(#62208,#62209,#62210),.UNSPECIFIED.,.F.,.F.)
B_SPLINE_CURVE_WITH_KNOTS((3,3),(0.280206015619895,0.367357794870771),
 .UNSPECIFIED.)
CURVE()
GEOMETRIC_REPRESENTATION_ITEM()
RATIONAL_B_SPLINE_CURVE((1.00589416567692,1.0061116250567,1.00589416567692))
REPRESENTATION_ITEM('')
);
#207=(
BOUNDED_CURVE()
B_SPLINE_CURVE(2,(#62214,#62215,#62216),.UNSPECIFIED.,.F.,.F.)
B_SPLINE_CURVE_WITH_KNOTS((3,3),(0.196145060700812,2.27801504598277),
 .UNSPECIFIED.)
CURVE()
GEOMETRIC_REPRESENTATION_ITEM()
RATIONAL_B_SPLINE_CURVE((1.02999692649796,1.1754825255573,1.02999692649702))
REPRESENTATION_ITEM('')
);
#208=(
BOUNDED_CURVE()
B_SPLINE_CURVE(2,(#62227,#62228,#62229),.UNSPECIFIED.,.F.,.F.)
B_SPLINE_CURVE_WITH_KNOTS((3,3),(0.196145060700811,1.23708005334447),
 .UNSPECIFIED.)
CURVE()
GEOMETRIC_REPRESENTATION_ITEM()
RATIONAL_B_SPLINE_CURVE((1.02999692649796,1.10273972602782,1.1027397260274))
REPRESENTATION_ITEM('')
);
#209=(
BOUNDED_CURVE()
B_SPLINE_CURVE(2,(#62231,#62232,#62233),.UNSPECIFIED.,.F.,.F.)
B_SPLINE_CURVE_WITH_KNOTS((3,3),(0.280206015619894,0.367357794870769),
 .UNSPECIFIED.)
CURVE()
GEOMETRIC_REPRESENTATION_ITEM()
RATIONAL_B_SPLINE_CURVE((1.00589416567691,1.00611162505669,1.00589416567691))
REPRESENTATION_ITEM('')
);
#210=(
BOUNDED_CURVE()
B_SPLINE_CURVE(2,(#62235,#62236,#62237),.UNSPECIFIED.,.F.,.F.)
B_SPLINE_CURVE_WITH_KNOTS((3,3),(0.196145060700811,2.27801504598277),
 .UNSPECIFIED.)
CURVE()
GEOMETRIC_REPRESENTATION_ITEM()
RATIONAL_B_SPLINE_CURVE((1.02999692649796,1.17548252555731,1.02999692649702))
REPRESENTATION_ITEM('')
);
#211=(
BOUNDED_CURVE()
B_SPLINE_CURVE(2,(#62239,#62240,#62241),.UNSPECIFIED.,.F.,.F.)
B_SPLINE_CURVE_WITH_KNOTS((3,3),(0.280206015619887,0.367357794870763),
 .UNSPECIFIED.)
CURVE()
GEOMETRIC_REPRESENTATION_ITEM()
RATIONAL_B_SPLINE_CURVE((1.00589416567691,1.00611162505669,1.00589416567691))
REPRESENTATION_ITEM('')
);
#212=(
BOUNDED_CURVE()
B_SPLINE_CURVE(2,(#62243,#62244,#62245),.UNSPECIFIED.,.F.,.F.)
B_SPLINE_CURVE_WITH_KNOTS((3,3),(0.196145060700811,2.27801504598277),
 .UNSPECIFIED.)
CURVE()
GEOMETRIC_REPRESENTATION_ITEM()
RATIONAL_B_SPLINE_CURVE((1.02999692649796,1.1754825255573,1.02999692649702))
REPRESENTATION_ITEM('')
);
#213=(
BOUNDED_CURVE()
B_SPLINE_CURVE(2,(#62247,#62248,#62249),.UNSPECIFIED.,.F.,.F.)
B_SPLINE_CURVE_WITH_KNOTS((3,3),(0.280206015619889,0.367357794870765),
 .UNSPECIFIED.)
CURVE()
GEOMETRIC_REPRESENTATION_ITEM()
RATIONAL_B_SPLINE_CURVE((1.00589416567691,1.00611162505669,1.00589416567691))
REPRESENTATION_ITEM('')
);
#214=(
BOUNDED_CURVE()
B_SPLINE_CURVE(2,(#62251,#62252,#62253),.UNSPECIFIED.,.F.,.F.)
B_SPLINE_CURVE_WITH_KNOTS((3,3),(0.196145060700811,2.27801504598277),
 .UNSPECIFIED.)
CURVE()
GEOMETRIC_REPRESENTATION_ITEM()
RATIONAL_B_SPLINE_CURVE((1.02999692649796,1.17548252555731,1.02999692649702))
REPRESENTATION_ITEM('')
);
#215=(
BOUNDED_CURVE()
B_SPLINE_CURVE(2,(#62254,#62255,#62256),.UNSPECIFIED.,.F.,.F.)
B_SPLINE_CURVE_WITH_KNOTS((3,3),(0.280206015619893,0.367357794870768),
 .UNSPECIFIED.)
CURVE()
GEOMETRIC_REPRESENTATION_ITEM()
RATIONAL_B_SPLINE_CURVE((1.00589416567691,1.00611162505669,1.00589416567691))
REPRESENTATION_ITEM('')
);
#216=(
BOUNDED_CURVE()
B_SPLINE_CURVE(2,(#62257,#62258,#62259),.UNSPECIFIED.,.F.,.F.)
B_SPLINE_CURVE_WITH_KNOTS((3,3),(1.23708005334447,2.27801504598277),
 .UNSPECIFIED.)
CURVE()
GEOMETRIC_REPRESENTATION_ITEM()
RATIONAL_B_SPLINE_CURVE((1.1027397260274,1.10273972602697,1.02999692649702))
REPRESENTATION_ITEM('')
);
#217=(
BOUNDED_CURVE()
B_SPLINE_CURVE(2,(#62263,#62264,#62265),.UNSPECIFIED.,.F.,.F.)
B_SPLINE_CURVE_WITH_KNOTS((3,3),(0.0551833308085754,0.208603356030846),
 .UNSPECIFIED.)
CURVE()
GEOMETRIC_REPRESENTATION_ITEM()
RATIONAL_B_SPLINE_CURVE((1.00066796366419,1.00140515246646,1.00107839993824))
REPRESENTATION_ITEM('')
);
#218=(
BOUNDED_CURVE()
B_SPLINE_CURVE(2,(#62269,#62270,#62271),.UNSPECIFIED.,.F.,.F.)
B_SPLINE_CURVE_WITH_KNOTS((3,3),(0.,0.0415381994417462),.UNSPECIFIED.)
CURVE()
GEOMETRIC_REPRESENTATION_ITEM()
RATIONAL_B_SPLINE_CURVE((1.,1.,1.))
REPRESENTATION_ITEM('')
);
#219=(
BOUNDED_CURVE()
B_SPLINE_CURVE(2,(#62283,#62284,#62285),.UNSPECIFIED.,.F.,.F.)
B_SPLINE_CURVE_WITH_KNOTS((3,3),(0.146737168364576,0.166814895714678),
 .UNSPECIFIED.)
CURVE()
GEOMETRIC_REPRESENTATION_ITEM()
RATIONAL_B_SPLINE_CURVE((1.00169850872058,1.00172953563951,1.001737254019))
REPRESENTATION_ITEM('')
);
#220=(
BOUNDED_CURVE()
B_SPLINE_CURVE(2,(#62287,#62288,#62289),.UNSPECIFIED.,.F.,.F.)
B_SPLINE_CURVE_WITH_KNOTS((3,3),(0.0286170700108412,0.076212379983174),
 .UNSPECIFIED.)
CURVE()
GEOMETRIC_REPRESENTATION_ITEM()
RATIONAL_B_SPLINE_CURVE((1.00112886559711,1.00201824869615,1.0027434105643))
REPRESENTATION_ITEM('')
);
#221=(
BOUNDED_CURVE()
B_SPLINE_CURVE(2,(#62291,#62292,#62293),.UNSPECIFIED.,.F.,.F.)
B_SPLINE_CURVE_WITH_KNOTS((3,3),(0.460004626021661,2.01415548066414),
 .UNSPECIFIED.)
CURVE()
GEOMETRIC_REPRESENTATION_ITEM()
RATIONAL_B_SPLINE_CURVE((1.06220108868579,1.14327836336948,1.06220108868485))
REPRESENTATION_ITEM('')
);
#222=(
BOUNDED_CURVE()
B_SPLINE_CURVE(2,(#62295,#62296,#62297),.UNSPECIFIED.,.F.,.F.)
B_SPLINE_CURVE_WITH_KNOTS((3,3),(0.517898922485178,0.565329042615561),
 .UNSPECIFIED.)
CURVE()
GEOMETRIC_REPRESENTATION_ITEM()
RATIONAL_B_SPLINE_CURVE((1.00287035745075,1.00210549051842,1.00117645345012))
REPRESENTATION_ITEM('')
);
#223=(
BOUNDED_CURVE()
B_SPLINE_CURVE(2,(#62299,#62300,#62301),.UNSPECIFIED.,.F.,.F.)
B_SPLINE_CURVE_WITH_KNOTS((3,3),(0.180111955289092,0.200189682639419),
 .UNSPECIFIED.)
CURVE()
GEOMETRIC_REPRESENTATION_ITEM()
RATIONAL_B_SPLINE_CURVE((1.00173725404747,1.00172953566789,1.0016985087485))
REPRESENTATION_ITEM('')
);
#224=(
BOUNDED_CURVE()
B_SPLINE_CURVE(2,(#62302,#62303,#62304),.UNSPECIFIED.,.F.,.F.)
B_SPLINE_CURVE_WITH_KNOTS((3,3),(0.13571848159483,0.289180967053278),
 .UNSPECIFIED.)
CURVE()
GEOMETRIC_REPRESENTATION_ITEM()
RATIONAL_B_SPLINE_CURVE((1.00140882605982,1.00173471838467,1.00099631962981))
REPRESENTATION_ITEM('')
);
#225=(
BOUNDED_CURVE()
B_SPLINE_CURVE(2,(#62309,#62310,#62311),.UNSPECIFIED.,.F.,.F.)
B_SPLINE_CURVE_WITH_KNOTS((3,3),(-2.1703979840528,-2.16974314947153),
 .UNSPECIFIED.)
CURVE()
GEOMETRIC_REPRESENTATION_ITEM()
RATIONAL_B_SPLINE_CURVE((1.2052492603669,1.20540347259793,1.20555757308984))
REPRESENTATION_ITEM('')
);
#226=(
BOUNDED_CURVE()
B_SPLINE_CURVE(2,(#62366,#62367,#62368),.UNSPECIFIED.,.F.,.F.)
B_SPLINE_CURVE_WITH_KNOTS((3,3),(-0.363565876377545,-0.362911041796268),
 .UNSPECIFIED.)
CURVE()
GEOMETRIC_REPRESENTATION_ITEM()
RATIONAL_B_SPLINE_CURVE((1.20555757308984,1.20540347259793,1.2052492603669))
REPRESENTATION_ITEM('')
);
#227=(
BOUNDED_CURVE()
B_SPLINE_CURVE(2,(#62388,#62389,#62390),.UNSPECIFIED.,.F.,.F.)
B_SPLINE_CURVE_WITH_KNOTS((3,3),(0.0400329798994461,0.0815711793412183),
 .UNSPECIFIED.)
CURVE()
GEOMETRIC_REPRESENTATION_ITEM()
RATIONAL_B_SPLINE_CURVE((1.,1.,1.))
REPRESENTATION_ITEM('')
);
#228=(
BOUNDED_CURVE()
B_SPLINE_CURVE(2,(#62421,#62422,#62423),.UNSPECIFIED.,.F.,.F.)
B_SPLINE_CURVE_WITH_KNOTS((3,3),(0.496551500635133,0.54414681060686),
 .UNSPECIFIED.)
CURVE()
GEOMETRIC_REPRESENTATION_ITEM()
RATIONAL_B_SPLINE_CURVE((1.00274341056425,1.00201824869611,1.00112886559708))
REPRESENTATION_ITEM('')
);
#229=(
BOUNDED_CURVE()
B_SPLINE_CURVE(2,(#62426,#62427,#62428),.UNSPECIFIED.,.F.,.F.)
B_SPLINE_CURVE_WITH_KNOTS((3,3),(0.180111955327547,0.200189682676742),
 .UNSPECIFIED.)
CURVE()
GEOMETRIC_REPRESENTATION_ITEM()
RATIONAL_B_SPLINE_CURVE((1.00173725401411,1.00172953563463,1.00169850871579))
REPRESENTATION_ITEM('')
);
#230=(
BOUNDED_CURVE()
B_SPLINE_CURVE(2,(#62430,#62431,#62432),.UNSPECIFIED.,.F.,.F.)
B_SPLINE_CURVE_WITH_KNOTS((3,3),(0.135718481594802,0.28918096705326),
 .UNSPECIFIED.)
CURVE()
GEOMETRIC_REPRESENTATION_ITEM()
RATIONAL_B_SPLINE_CURVE((1.00140882605999,1.00173471838487,1.00099631962993))
REPRESENTATION_ITEM('')
);
#231=(
BOUNDED_CURVE()
B_SPLINE_CURVE(2,(#62436,#62437,#62438),.UNSPECIFIED.,.F.,.F.)
B_SPLINE_CURVE_WITH_KNOTS((3,3),(0.0762382668082746,0.229700752266092),
 .UNSPECIFIED.)
CURVE()
GEOMETRIC_REPRESENTATION_ITEM()
RATIONAL_B_SPLINE_CURVE((1.00099631962987,1.00173471838476,1.0014088260599))
REPRESENTATION_ITEM('')
);
#232=(
BOUNDED_CURVE()
B_SPLINE_CURVE(2,(#62440,#62441,#62442),.UNSPECIFIED.,.F.,.F.)
B_SPLINE_CURVE_WITH_KNOTS((3,3),(0.146737168364582,0.166814895714678),
 .UNSPECIFIED.)
CURVE()
GEOMETRIC_REPRESENTATION_ITEM()
RATIONAL_B_SPLINE_CURVE((1.00169850872035,1.00172953563927,1.00173725401877))
REPRESENTATION_ITEM('')
);
#233=(
BOUNDED_CURVE()
B_SPLINE_CURVE(2,(#62443,#62444,#62445),.UNSPECIFIED.,.F.,.F.)
B_SPLINE_CURVE_WITH_KNOTS((3,3),(0.0285159432695787,0.075946063400608),
 .UNSPECIFIED.)
CURVE()
GEOMETRIC_REPRESENTATION_ITEM()
RATIONAL_B_SPLINE_CURVE((1.00117645345009,1.00210549051841,1.00287035745075))
REPRESENTATION_ITEM('')
);
#234=(
BOUNDED_CURVE()
B_SPLINE_CURVE(2,(#62450,#62451,#62452),.UNSPECIFIED.,.F.,.F.)
B_SPLINE_CURVE_WITH_KNOTS((3,3),(-0.363565876377541,-0.362911041796264),
 .UNSPECIFIED.)
CURVE()
GEOMETRIC_REPRESENTATION_ITEM()
RATIONAL_B_SPLINE_CURVE((1.20555757308984,1.20540347259794,1.2052492603669))
REPRESENTATION_ITEM('')
);
#235=(
BOUNDED_CURVE()
B_SPLINE_CURVE(2,(#62464,#62465,#62466),.UNSPECIFIED.,.F.,.F.)
B_SPLINE_CURVE_WITH_KNOTS((3,3),(0.460004626021663,2.01415548066414),
 .UNSPECIFIED.)
CURVE()
GEOMETRIC_REPRESENTATION_ITEM()
RATIONAL_B_SPLINE_CURVE((1.06220108868579,1.14327836336948,1.06220108868485))
REPRESENTATION_ITEM('')
);
#236=(
BOUNDED_CURVE()
B_SPLINE_CURVE(2,(#62480,#62481,#62482),.UNSPECIFIED.,.F.,.F.)
B_SPLINE_CURVE_WITH_KNOTS((3,3),(0.496551500635129,0.544146810606855),
 .UNSPECIFIED.)
CURVE()
GEOMETRIC_REPRESENTATION_ITEM()
RATIONAL_B_SPLINE_CURVE((1.00274341056426,1.00201824869612,1.00112886559708))
REPRESENTATION_ITEM('')
);
#237=(
BOUNDED_CURVE()
B_SPLINE_CURVE(2,(#62488,#62489,#62490),.UNSPECIFIED.,.F.,.F.)
B_SPLINE_CURVE_WITH_KNOTS((3,3),(-0.363565876377545,-0.362911041796268),
 .UNSPECIFIED.)
CURVE()
GEOMETRIC_REPRESENTATION_ITEM()
RATIONAL_B_SPLINE_CURVE((1.20555757308984,1.20540347259793,1.2052492603669))
REPRESENTATION_ITEM('')
);
#238=(
BOUNDED_CURVE()
B_SPLINE_CURVE(2,(#62495,#62496,#62497),.UNSPECIFIED.,.F.,.F.)
B_SPLINE_CURVE_WITH_KNOTS((3,3),(0.180111955326739,0.200189682676032),
 .UNSPECIFIED.)
CURVE()
GEOMETRIC_REPRESENTATION_ITEM()
RATIONAL_B_SPLINE_CURVE((1.00173725401877,1.00172953563927,1.00169850872035))
REPRESENTATION_ITEM('')
);
#239=(
BOUNDED_CURVE()
B_SPLINE_CURVE(2,(#62506,#62507,#62508),.UNSPECIFIED.,.F.,.F.)
B_SPLINE_CURVE_WITH_KNOTS((3,3),(-2.1703979840528,-2.16974314947152),
 .UNSPECIFIED.)
CURVE()
GEOMETRIC_REPRESENTATION_ITEM()
RATIONAL_B_SPLINE_CURVE((1.2052492603669,1.20540347259793,1.20555757308983))
REPRESENTATION_ITEM('')
);
#240=(
BOUNDED_CURVE()
B_SPLINE_CURVE(2,(#62514,#62515,#62516),.UNSPECIFIED.,.F.,.F.)
B_SPLINE_CURVE_WITH_KNOTS((3,3),(0.,0.0415381989501033),.UNSPECIFIED.)
CURVE()
GEOMETRIC_REPRESENTATION_ITEM()
RATIONAL_B_SPLINE_CURVE((1.,1.,1.))
REPRESENTATION_ITEM('')
);
#241=(
BOUNDED_CURVE()
B_SPLINE_CURVE(2,(#62522,#62523,#62524),.UNSPECIFIED.,.F.,.F.)
B_SPLINE_CURVE_WITH_KNOTS((3,3),(2.58081477858363,2.59739059715085),
 .UNSPECIFIED.)
CURVE()
GEOMETRIC_REPRESENTATION_ITEM()
RATIONAL_B_SPLINE_CURVE((1.03637289268669,1.01830325256961,1.))
REPRESENTATION_ITEM('')
);
#242=(
BOUNDED_CURVE()
B_SPLINE_CURVE(2,(#62527,#62528,#62529),.UNSPECIFIED.,.F.,.F.)
B_SPLINE_CURVE_WITH_KNOTS((3,3),(1.77226571272999,1.80534191248319),
 .UNSPECIFIED.)
CURVE()
GEOMETRIC_REPRESENTATION_ITEM()
RATIONAL_B_SPLINE_CURVE((1.0219180827151,1.01662663545196,1.01113004279036))
REPRESENTATION_ITEM('')
);
#243=(
BOUNDED_CURVE()
B_SPLINE_CURVE(2,(#62587,#62588,#62589),.UNSPECIFIED.,.F.,.F.)
B_SPLINE_CURVE_WITH_KNOTS((3,3),(0.0468703348388751,0.0935146604975977),
 .UNSPECIFIED.)
CURVE()
GEOMETRIC_REPRESENTATION_ITEM()
RATIONAL_B_SPLINE_CURVE((1.00023109890562,1.00023054172511,1.))
REPRESENTATION_ITEM('')
);
#244=(
BOUNDED_CURVE()
B_SPLINE_CURVE(2,(#62597,#62598,#62599),.UNSPECIFIED.,.F.,.F.)
B_SPLINE_CURVE_WITH_KNOTS((3,3),(-2.1703979840528,-2.16974314947153),
 .UNSPECIFIED.)
CURVE()
GEOMETRIC_REPRESENTATION_ITEM()
RATIONAL_B_SPLINE_CURVE((1.2052492603669,1.20540347259793,1.20555757308984))
REPRESENTATION_ITEM('')
);
#245=(
BOUNDED_CURVE()
B_SPLINE_CURVE(2,(#62605,#62606,#62607),.UNSPECIFIED.,.F.,.F.)
B_SPLINE_CURVE_WITH_KNOTS((3,3),(-0.363565876377547,-0.36291104179627),
 .UNSPECIFIED.)
CURVE()
GEOMETRIC_REPRESENTATION_ITEM()
RATIONAL_B_SPLINE_CURVE((1.20555757308984,1.20540347259793,1.2052492603669))
REPRESENTATION_ITEM('')
);
#246=(
BOUNDED_CURVE()
B_SPLINE_CURVE(2,(#62618,#62619,#62620),.UNSPECIFIED.,.F.,.F.)
B_SPLINE_CURVE_WITH_KNOTS((3,3),(-2.17039798405279,-2.16974314947152),
 .UNSPECIFIED.)
CURVE()
GEOMETRIC_REPRESENTATION_ITEM()
RATIONAL_B_SPLINE_CURVE((1.20524926036689,1.20540347259792,1.20555757308983))
REPRESENTATION_ITEM('')
);
#247=(
BOUNDED_CURVE()
B_SPLINE_CURVE(2,(#62660,#62661,#62662),.UNSPECIFIED.,.F.,.F.)
B_SPLINE_CURVE_WITH_KNOTS((3,3),(2.58081477858368,2.5973905971509),
 .UNSPECIFIED.)
CURVE()
GEOMETRIC_REPRESENTATION_ITEM()
RATIONAL_B_SPLINE_CURVE((1.03637289268669,1.01830325256961,1.))
REPRESENTATION_ITEM('')
);
#248=(
BOUNDED_CURVE()
B_SPLINE_CURVE(2,(#62667,#62668,#62669),.UNSPECIFIED.,.F.,.F.)
B_SPLINE_CURVE_WITH_KNOTS((3,3),(0.0764015610922613,0.230183975191949),
 .UNSPECIFIED.)
CURVE()
GEOMETRIC_REPRESENTATION_ITEM()
RATIONAL_B_SPLINE_CURVE((1.00095841961808,1.00165861973304,1.001294595355))
REPRESENTATION_ITEM('')
);
#249=(
BOUNDED_CURVE()
B_SPLINE_CURVE(2,(#62675,#62676,#62677),.UNSPECIFIED.,.F.,.F.)
B_SPLINE_CURVE_WITH_KNOTS((3,3),(0.0286170700108397,0.0762123799831708),
 .UNSPECIFIED.)
CURVE()
GEOMETRIC_REPRESENTATION_ITEM()
RATIONAL_B_SPLINE_CURVE((1.00112886559711,1.00201824869616,1.00274341056431))
REPRESENTATION_ITEM('')
);
#250=(
BOUNDED_CURVE()
B_SPLINE_CURVE(2,(#62683,#62684,#62685),.UNSPECIFIED.,.F.,.F.)
B_SPLINE_CURVE_WITH_KNOTS((3,3),(0.460004626021665,2.01415548066414),
 .UNSPECIFIED.)
CURVE()
GEOMETRIC_REPRESENTATION_ITEM()
RATIONAL_B_SPLINE_CURVE((1.06220108868579,1.14327836336947,1.06220108868485))
REPRESENTATION_ITEM('')
);
#251=(
BOUNDED_CURVE()
B_SPLINE_CURVE(2,(#62687,#62688,#62689),.UNSPECIFIED.,.F.,.F.)
B_SPLINE_CURVE_WITH_KNOTS((3,3),(0.517898922485166,0.565329042615548),
 .UNSPECIFIED.)
CURVE()
GEOMETRIC_REPRESENTATION_ITEM()
RATIONAL_B_SPLINE_CURVE((1.00287035745074,1.00210549051841,1.00117645345011))
REPRESENTATION_ITEM('')
);
#252=(
BOUNDED_CURVE()
B_SPLINE_CURVE(2,(#62691,#62692,#62693),.UNSPECIFIED.,.F.,.F.)
B_SPLINE_CURVE_WITH_KNOTS((3,3),(0.180111955322879,0.20018968267217),
 .UNSPECIFIED.)
CURVE()
GEOMETRIC_REPRESENTATION_ITEM()
RATIONAL_B_SPLINE_CURVE((1.00173725401601,1.00172953563653,1.00169850871767))
REPRESENTATION_ITEM('')
);
#253=(
BOUNDED_CURVE()
B_SPLINE_CURVE(2,(#62695,#62696,#62697),.UNSPECIFIED.,.F.,.F.)
B_SPLINE_CURVE_WITH_KNOTS((3,3),(0.12497957891104,0.278761993011364),
 .UNSPECIFIED.)
CURVE()
GEOMETRIC_REPRESENTATION_ITEM()
RATIONAL_B_SPLINE_CURVE((1.00129459535509,1.00165861973317,1.00095841961815))
REPRESENTATION_ITEM('')
);
#254=(
BOUNDED_CURVE()
B_SPLINE_CURVE(2,(#62699,#62700,#62701),.UNSPECIFIED.,.F.,.F.)
B_SPLINE_CURVE_WITH_KNOTS((3,3),(0.146737168401206,0.166814895752325),
 .UNSPECIFIED.)
CURVE()
GEOMETRIC_REPRESENTATION_ITEM()
RATIONAL_B_SPLINE_CURVE((1.00169850874789,1.00172953566728,1.00173725404685))
REPRESENTATION_ITEM('')
);
#255=(
BOUNDED_CURVE()
B_SPLINE_CURVE(2,(#62711,#62712,#62713),.UNSPECIFIED.,.F.,.F.)
B_SPLINE_CURVE_WITH_KNOTS((3,3),(2.58081477858364,2.59739059715087),
 .UNSPECIFIED.)
CURVE()
GEOMETRIC_REPRESENTATION_ITEM()
RATIONAL_B_SPLINE_CURVE((1.03637289268669,1.01830325256961,1.))
REPRESENTATION_ITEM('')
);
#256=(
BOUNDED_CURVE()
B_SPLINE_CURVE(2,(#62717,#62718,#62719),.UNSPECIFIED.,.F.,.F.)
B_SPLINE_CURVE_WITH_KNOTS((3,3),(0.,0.0165758185672203),.UNSPECIFIED.)
CURVE()
GEOMETRIC_REPRESENTATION_ITEM()
RATIONAL_B_SPLINE_CURVE((1.,1.01830325256961,1.03637289268669))
REPRESENTATION_ITEM('')
);
#257=(
BOUNDED_CURVE()
B_SPLINE_CURVE(2,(#62746,#62747,#62748),.UNSPECIFIED.,.F.,.F.)
B_SPLINE_CURVE_WITH_KNOTS((3,3),(-0.363565876377549,-0.362911041796272),
 .UNSPECIFIED.)
CURVE()
GEOMETRIC_REPRESENTATION_ITEM()
RATIONAL_B_SPLINE_CURVE((1.20555757308984,1.20540347259793,1.2052492603669))
REPRESENTATION_ITEM('')
);
#258=(
BOUNDED_CURVE()
B_SPLINE_CURVE(2,(#62751,#62752,#62753),.UNSPECIFIED.,.F.,.F.)
B_SPLINE_CURVE_WITH_KNOTS((3,3),(-2.17039798405279,-2.16974314947152),
 .UNSPECIFIED.)
CURVE()
GEOMETRIC_REPRESENTATION_ITEM()
RATIONAL_B_SPLINE_CURVE((1.20524926036689,1.20540347259792,1.20555757308982))
REPRESENTATION_ITEM('')
);
#259=(
BOUNDED_CURVE()
B_SPLINE_CURVE(2,(#62757,#62758,#62759),.UNSPECIFIED.,.F.,.F.)
B_SPLINE_CURVE_WITH_KNOTS((3,3),(0.0764015610913054,0.230183975191003),
 .UNSPECIFIED.)
CURVE()
GEOMETRIC_REPRESENTATION_ITEM()
RATIONAL_B_SPLINE_CURVE((1.00095841961842,1.00165861973365,1.00129459535547))
REPRESENTATION_ITEM('')
);
#260=(
BOUNDED_CURVE()
B_SPLINE_CURVE(2,(#62766,#62767,#62768),.UNSPECIFIED.,.F.,.F.)
B_SPLINE_CURVE_WITH_KNOTS((3,3),(0.1249795789111,0.278761993011415),
 .UNSPECIFIED.)
CURVE()
GEOMETRIC_REPRESENTATION_ITEM()
RATIONAL_B_SPLINE_CURVE((1.00129459535522,1.00165861973333,1.00095841961823))
REPRESENTATION_ITEM('')
);
#261=(
BOUNDED_CURVE()
B_SPLINE_CURVE(2,(#62781,#62782,#62783),.UNSPECIFIED.,.F.,.F.)
B_SPLINE_CURVE_WITH_KNOTS((3,3),(0.0285159432695794,0.0759460634006091),
 .UNSPECIFIED.)
CURVE()
GEOMETRIC_REPRESENTATION_ITEM()
RATIONAL_B_SPLINE_CURVE((1.00117645345008,1.00210549051839,1.00287035745073))
REPRESENTATION_ITEM('')
);
#262=(
BOUNDED_CURVE()
B_SPLINE_CURVE(2,(#62807,#62808,#62809),.UNSPECIFIED.,.F.,.F.)
B_SPLINE_CURVE_WITH_KNOTS((3,3),(0.146737168363879,0.166814895713834),
 .UNSPECIFIED.)
CURVE()
GEOMETRIC_REPRESENTATION_ITEM()
RATIONAL_B_SPLINE_CURVE((1.00169850871386,1.00172953563266,1.00173725401213))
REPRESENTATION_ITEM('')
);
#303=SHAPE_REPRESENTATION_RELATIONSHIP('SRR','None',#71691,#316);
#316=ADVANCED_BREP_SHAPE_REPRESENTATION('',(#342),#71623);
#329=STYLED_ITEM('',(#71825),#342);
#342=MANIFOLD_SOLID_BREP('Body1',#34216);
#655=B_SPLINE_CURVE_WITH_KNOTS('',3,(#62088,#62089,#62090,#62091),
 .UNSPECIFIED.,.F.,.F.,(4,4),(0.0459042098603345,0.091874680867398),
 .UNSPECIFIED.);
#656=B_SPLINE_CURVE_WITH_KNOTS('',3,(#62094,#62095,#62096,#62097),
 .UNSPECIFIED.,.F.,.F.,(4,4),(0.0459042098603146,0.0918746808673364),
 .UNSPECIFIED.);
#657=B_SPLINE_CURVE_WITH_KNOTS('',3,(#62163,#62164,#62165,#62166),
 .UNSPECIFIED.,.F.,.F.,(4,4),(0.0459042098603271,0.0918746808673741),
 .UNSPECIFIED.);
#658=B_SPLINE_CURVE_WITH_KNOTS('',3,(#62169,#62170,#62171,#62172),
 .UNSPECIFIED.,.F.,.F.,(4,4),(0.,0.0459735749039228),.UNSPECIFIED.);
#659=B_SPLINE_CURVE_WITH_KNOTS('',3,(#62394,#62395,#62396,#62397),
 .UNSPECIFIED.,.F.,.F.,(4,4),(0.0459042098603282,0.0918746808673777),
 .UNSPECIFIED.);
#660=B_SPLINE_CURVE_WITH_KNOTS('',3,(#62400,#62401,#62402,#62403),
 .UNSPECIFIED.,.F.,.F.,(4,4),(0.04590420986033,0.0918746808673833),
 .UNSPECIFIED.);
#661=B_SPLINE_CURVE_WITH_KNOTS('',3,(#62539,#62540,#62541,#62542),
 .UNSPECIFIED.,.F.,.F.,(4,4),(-0.0918808841872258,0.),.UNSPECIFIED.);
#662=B_SPLINE_CURVE_WITH_KNOTS('',3,(#62546,#62547,#62548,#62549),
 .UNSPECIFIED.,.F.,.F.,(4,4),(-0.0918746808673604,0.),.UNSPECIFIED.);
#663=B_SPLINE_CURVE_WITH_KNOTS('',3,(#62552,#62553,#62554,#62555),
 .UNSPECIFIED.,.F.,.F.,(4,4),(-0.0918808841872082,0.),.UNSPECIFIED.);
#664=B_SPLINE_CURVE_WITH_KNOTS('',3,(#62561,#62562,#62563,#62564),
 .UNSPECIFIED.,.F.,.F.,(4,4),(-0.0918808841872279,0.),.UNSPECIFIED.);
#665=B_SPLINE_CURVE_WITH_KNOTS('',3,(#62569,#62570,#62571,#62572),
 .UNSPECIFIED.,.F.,.F.,(4,4),(-0.0918746808673616,0.),.UNSPECIFIED.);
#666=B_SPLINE_CURVE_WITH_KNOTS('',3,(#62575,#62576,#62577,#62578),
 .UNSPECIFIED.,.F.,.F.,(4,4),(-0.0918808841872121,0.),.UNSPECIFIED.);
#667=B_SPLINE_CURVE_WITH_KNOTS('',3,(#62592,#62593,#62594,#62595),
 .UNSPECIFIED.,.F.,.F.,(4,4),(-0.0918746808673705,0.),.UNSPECIFIED.);
#668=B_SPLINE_CURVE_WITH_KNOTS('',3,(#62612,#62613,#62614,#62615),
 .UNSPECIFIED.,.F.,.F.,(4,4),(-0.0918746808673773,0.),.UNSPECIFIED.);
#669=B_SPLINE_CURVE_WITH_KNOTS('',3,(#62627,#62628,#62629,#62630),
 .UNSPECIFIED.,.F.,.F.,(4,4),(-0.0918746808673589,0.),.UNSPECIFIED.);
#670=B_SPLINE_CURVE_WITH_KNOTS('',3,(#62654,#62655,#62656,#62657),
 .UNSPECIFIED.,.F.,.F.,(4,4),(0.,0.0417760674242005),.UNSPECIFIED.);
#671=B_SPLINE_CURVE_WITH_KNOTS('',3,(#62726,#62727,#62728,#62729),
 .UNSPECIFIED.,.F.,.F.,(4,4),(-0.0918746808673938,0.),.UNSPECIFIED.);
#672=B_SPLINE_CURVE_WITH_KNOTS('',3,(#62740,#62741,#62742,#62743),
 .UNSPECIFIED.,.F.,.F.,(4,4),(-0.0918808841872246,0.),.UNSPECIFIED.);
#673=B_SPLINE_CURVE_WITH_KNOTS('',3,(#62771,#62772,#62773,#62774),
 .UNSPECIFIED.,.F.,.F.,(4,4),(-0.0918808841872257,0.),.UNSPECIFIED.);
#1292=FACE_BOUND('',#7179,.T.);
#2698=PLANE('',#37038);
#2699=PLANE('',#37039);
#2700=PLANE('',#37043);
#2701=PLANE('',#37044);
#2702=PLANE('',#37045);
#2703=PLANE('',#37046);
#2704=PLANE('',#37047);
#2705=PLANE('',#37048);
#2706=PLANE('',#37050);
#2707=PLANE('',#37051);
#2708=PLANE('',#37054);
#2709=PLANE('',#37055);
#2710=PLANE('',#37056);
#2711=PLANE('',#37057);
#2712=PLANE('',#37058);
#2713=PLANE('',#37062);
#2714=PLANE('',#37065);
#2715=PLANE('',#37066);
#2716=PLANE('',#37067);
#2717=PLANE('',#37070);
#2718=PLANE('',#37071);
#2719=PLANE('',#37075);
#2720=PLANE('',#37076);
#2721=PLANE('',#37077);
#2722=PLANE('',#37078);
#2723=PLANE('',#37079);
#2724=PLANE('',#37080);
#2725=PLANE('',#37081);
#2726=PLANE('',#37082);
#2727=PLANE('',#37083);
#2728=PLANE('',#37084);
#2729=PLANE('',#37085);
#2730=PLANE('',#37086);
#2731=PLANE('',#37087);
#2732=PLANE('',#37089);
#2733=PLANE('',#37090);
#2734=PLANE('',#37093);
#2735=PLANE('',#37094);
#2736=PLANE('',#37095);
#2737=PLANE('',#37098);
#2738=PLANE('',#37099);
#2739=PLANE('',#37101);
#2740=PLANE('',#37102);
#2741=PLANE('',#37103);
#2742=PLANE('',#37104);
#2743=PLANE('',#37105);
#2744=PLANE('',#37106);
#2745=PLANE('',#37107);
#2746=PLANE('',#37111);
#2747=PLANE('',#37112);
#2748=PLANE('',#37113);
#2749=PLANE('',#37114);
#2750=PLANE('',#37115);
#2751=PLANE('',#37116);
#2752=PLANE('',#37117);
#2753=PLANE('',#37118);
#2754=PLANE('',#37119);
#2755=PLANE('',#37120);
#2756=PLANE('',#37126);
#2757=PLANE('',#37131);
#2758=PLANE('',#37142);
#2759=PLANE('',#37143);
#2760=PLANE('',#37144);
#2761=PLANE('',#37147);
#2762=PLANE('',#37148);
#2763=PLANE('',#37149);
#2764=PLANE('',#37150);
#2765=PLANE('',#37151);
#2766=PLANE('',#37152);
#2767=PLANE('',#37153);
#2768=PLANE('',#37156);
#2769=PLANE('',#37159);
#2770=PLANE('',#37160);
#2771=PLANE('',#37163);
#2772=PLANE('',#37164);
#2773=PLANE('',#37165);
#2774=PLANE('',#37166);
#2775=PLANE('',#37167);
#2776=PLANE('',#37168);
#2777=PLANE('',#37169);
#2778=PLANE('',#37170);
#2779=PLANE('',#37175);
#2780=PLANE('',#37176);
#2781=PLANE('',#37177);
#2782=PLANE('',#37178);
#2783=PLANE('',#37179);
#2784=PLANE('',#37180);
#2785=PLANE('',#37181);
#2786=PLANE('',#37182);
#2787=PLANE('',#37183);
#2788=PLANE('',#37184);
#3070=CYLINDRICAL_SURFACE('',#37132,12.75);
#4810=FACE_OUTER_BOUND('',#7067,.T.);
#4811=FACE_OUTER_BOUND('',#7068,.T.);
#4812=FACE_OUTER_BOUND('',#7069,.T.);
#4813=FACE_OUTER_BOUND('',#7070,.T.);
#4814=FACE_OUTER_BOUND('',#7071,.T.);
#4815=FACE_OUTER_BOUND('',#7072,.T.);
#4816=FACE_OUTER_BOUND('',#7073,.T.);
#4817=FACE_OUTER_BOUND('',#7074,.T.);
#4818=FACE_OUTER_BOUND('',#7075,.T.);
#4819=FACE_OUTER_BOUND('',#7076,.T.);
#4820=FACE_OUTER_BOUND('',#7077,.T.);
#4821=FACE_OUTER_BOUND('',#7078,.T.);
#4822=FACE_OUTER_BOUND('',#7079,.T.);
#4823=FACE_OUTER_BOUND('',#7080,.T.);
#4824=FACE_OUTER_BOUND('',#7081,.T.);
#4825=FACE_OUTER_BOUND('',#7082,.T.);
#4826=FACE_OUTER_BOUND('',#7083,.T.);
#4827=FACE_OUTER_BOUND('',#7084,.T.);
#4828=FACE_OUTER_BOUND('',#7085,.T.);
#4829=FACE_OUTER_BOUND('',#7086,.T.);
#4830=FACE_OUTER_BOUND('',#7087,.T.);
#4831=FACE_OUTER_BOUND('',#7088,.T.);
#4832=FACE_OUTER_BOUND('',#7089,.T.);
#4833=FACE_OUTER_BOUND('',#7090,.T.);
#4834=FACE_OUTER_BOUND('',#7091,.T.);
#4835=FACE_OUTER_BOUND('',#7092,.T.);
#4836=FACE_OUTER_BOUND('',#7093,.T.);
#4837=FACE_OUTER_BOUND('',#7094,.T.);
#4838=FACE_OUTER_BOUND('',#7095,.T.);
#4839=FACE_OUTER_BOUND('',#7096,.T.);
#4840=FACE_OUTER_BOUND('',#7097,.T.);
#4841=FACE_OUTER_BOUND('',#7098,.T.);
#4842=FACE_OUTER_BOUND('',#7099,.T.);
#4843=FACE_OUTER_BOUND('',#7100,.T.);
#4844=FACE_OUTER_BOUND('',#7101,.T.);
#4845=FACE_OUTER_BOUND('',#7102,.T.);
#4846=FACE_OUTER_BOUND('',#7103,.T.);
#4847=FACE_OUTER_BOUND('',#7104,.T.);
#4848=FACE_OUTER_BOUND('',#7105,.T.);
#4849=FACE_OUTER_BOUND('',#7106,.T.);
#4850=FACE_OUTER_BOUND('',#7107,.T.);
#4851=FACE_OUTER_BOUND('',#7108,.T.);
#4852=FACE_OUTER_BOUND('',#7109,.T.);
#4853=FACE_OUTER_BOUND('',#7110,.T.);
#4854=FACE_OUTER_BOUND('',#7111,.T.);
#4855=FACE_OUTER_BOUND('',#7112,.T.);
#4856=FACE_OUTER_BOUND('',#7113,.T.);
#4857=FACE_OUTER_BOUND('',#7114,.T.);
#4858=FACE_OUTER_BOUND('',#7115,.T.);
#4859=FACE_OUTER_BOUND('',#7116,.T.);
#4860=FACE_OUTER_BOUND('',#7117,.T.);
#4861=FACE_OUTER_BOUND('',#7118,.T.);
#4862=FACE_OUTER_BOUND('',#7119,.T.);
#4863=FACE_OUTER_BOUND('',#7120,.T.);
#4864=FACE_OUTER_BOUND('',#7121,.T.);
#4865=FACE_OUTER_BOUND('',#7122,.T.);
#4866=FACE_OUTER_BOUND('',#7123,.T.);
#4867=FACE_OUTER_BOUND('',#7124,.T.);
#4868=FACE_OUTER_BOUND('',#7125,.T.);
#4869=FACE_OUTER_BOUND('',#7126,.T.);
#4870=FACE_OUTER_BOUND('',#7127,.T.);
#4871=FACE_OUTER_BOUND('',#7128,.T.);
#4872=FACE_OUTER_BOUND('',#7129,.T.);
#4873=FACE_OUTER_BOUND('',#7130,.T.);
#4874=FACE_OUTER_BOUND('',#7131,.T.);
#4875=FACE_OUTER_BOUND('',#7132,.T.);
#4876=FACE_OUTER_BOUND('',#7133,.T.);
#4877=FACE_OUTER_BOUND('',#7134,.T.);
#4878=FACE_OUTER_BOUND('',#7135,.T.);
#4879=FACE_OUTER_BOUND('',#7136,.T.);
#4880=FACE_OUTER_BOUND('',#7137,.T.);
#4881=FACE_OUTER_BOUND('',#7138,.T.);
#4882=FACE_OUTER_BOUND('',#7139,.T.);
#4883=FACE_OUTER_BOUND('',#7140,.T.);
#4884=FACE_OUTER_BOUND('',#7141,.T.);
#4885=FACE_OUTER_BOUND('',#7142,.T.);
#4886=FACE_OUTER_BOUND('',#7143,.T.);
#4887=FACE_OUTER_BOUND('',#7144,.T.);
#4888=FACE_OUTER_BOUND('',#7145,.T.);
#4889=FACE_OUTER_BOUND('',#7146,.T.);
#4890=FACE_OUTER_BOUND('',#7147,.T.);
#4891=FACE_OUTER_BOUND('',#7148,.T.);
#4892=FACE_OUTER_BOUND('',#7149,.T.);
#4893=FACE_OUTER_BOUND('',#7150,.T.);
#4894=FACE_OUTER_BOUND('',#7151,.T.);
#4895=FACE_OUTER_BOUND('',#7152,.T.);
#4896=FACE_OUTER_BOUND('',#7153,.T.);
#4897=FACE_OUTER_BOUND('',#7154,.T.);
#4898=FACE_OUTER_BOUND('',#7155,.T.);
#4899=FACE_OUTER_BOUND('',#7156,.T.);
#4900=FACE_OUTER_BOUND('',#7157,.T.);
#4901=FACE_OUTER_BOUND('',#7158,.T.);
#4902=FACE_OUTER_BOUND('',#7159,.T.);
#4903=FACE_OUTER_BOUND('',#7160,.T.);
#4904=FACE_OUTER_BOUND('',#7161,.T.);
#4905=FACE_OUTER_BOUND('',#7162,.T.);
#4906=FACE_OUTER_BOUND('',#7163,.T.);
#4907=FACE_OUTER_BOUND('',#7164,.T.);
#4908=FACE_OUTER_BOUND('',#7165,.T.);
#4909=FACE_OUTER_BOUND('',#7166,.T.);
#4910=FACE_OUTER_BOUND('',#7167,.T.);
#4911=FACE_OUTER_BOUND('',#7168,.T.);
#4912=FACE_OUTER_BOUND('',#7169,.T.);
#4913=FACE_OUTER_BOUND('',#7170,.T.);
#4914=FACE_OUTER_BOUND('',#7171,.T.);
#4915=FACE_OUTER_BOUND('',#7172,.T.);
#4916=FACE_OUTER_BOUND('',#7173,.T.);
#4917=FACE_OUTER_BOUND('',#7174,.T.);
#4918=FACE_OUTER_BOUND('',#7175,.T.);
#4919=FACE_OUTER_BOUND('',#7176,.T.);
#4920=FACE_OUTER_BOUND('',#7177,.T.);
#4921=FACE_OUTER_BOUND('',#7178,.T.);
#7067=EDGE_LOOP('',(#29802,#29803,#29804,#29805,#29806));
#7068=EDGE_LOOP('',(#29807,#29808,#29809,#29810));
#7069=EDGE_LOOP('',(#29811,#29812,#29813,#29814,#29815,#29816,#29817,#29818));
#7070=EDGE_LOOP('',(#29819,#29820,#29821,#29822,#29823,#29824,#29825));
#7071=EDGE_LOOP('',(#29826,#29827,#29828,#29829));
#7072=EDGE_LOOP('',(#29830,#29831,#29832,#29833));
#7073=EDGE_LOOP('',(#29834,#29835,#29836,#29837,#29838,#29839));
#7074=EDGE_LOOP('',(#29840,#29841,#29842,#29843,#29844,#29845,#29846));
#7075=EDGE_LOOP('',(#29847,#29848,#29849,#29850,#29851));
#7076=EDGE_LOOP('',(#29852,#29853,#29854,#29855,#29856,#29857));
#7077=EDGE_LOOP('',(#29858,#29859,#29860,#29861,#29862));
#7078=EDGE_LOOP('',(#29863,#29864,#29865,#29866,#29867,#29868));
#7079=EDGE_LOOP('',(#29869,#29870,#29871,#29872,#29873));
#7080=EDGE_LOOP('',(#29874,#29875,#29876,#29877,#29878,#29879,#29880,#29881));
#7081=EDGE_LOOP('',(#29882,#29883,#29884,#29885,#29886,#29887));
#7082=EDGE_LOOP('',(#29888,#29889,#29890,#29891,#29892,#29893));
#7083=EDGE_LOOP('',(#29894,#29895,#29896,#29897,#29898));
#7084=EDGE_LOOP('',(#29899,#29900,#29901,#29902,#29903,#29904));
#7085=EDGE_LOOP('',(#29905,#29906,#29907,#29908));
#7086=EDGE_LOOP('',(#29909,#29910,#29911,#29912,#29913,#29914,#29915,#29916));
#7087=EDGE_LOOP('',(#29917,#29918,#29919,#29920));
#7088=EDGE_LOOP('',(#29921,#29922,#29923,#29924,#29925));
#7089=EDGE_LOOP('',(#29926,#29927,#29928,#29929,#29930,#29931,#29932,#29933));
#7090=EDGE_LOOP('',(#29934,#29935,#29936,#29937,#29938,#29939,#29940,#29941,
#29942,#29943,#29944,#29945,#29946,#29947,#29948,#29949));
#7091=EDGE_LOOP('',(#29950,#29951,#29952,#29953,#29954));
#7092=EDGE_LOOP('',(#29955,#29956,#29957,#29958));
#7093=EDGE_LOOP('',(#29959,#29960,#29961,#29962,#29963,#29964,#29965,#29966));
#7094=EDGE_LOOP('',(#29967,#29968,#29969,#29970,#29971,#29972,#29973));
#7095=EDGE_LOOP('',(#29974,#29975,#29976,#29977));
#7096=EDGE_LOOP('',(#29978,#29979,#29980));
#7097=EDGE_LOOP('',(#29981,#29982,#29983,#29984,#29985));
#7098=EDGE_LOOP('',(#29986,#29987,#29988,#29989));
#7099=EDGE_LOOP('',(#29990,#29991,#29992,#29993,#29994));
#7100=EDGE_LOOP('',(#29995,#29996,#29997,#29998));
#7101=EDGE_LOOP('',(#29999,#30000,#30001,#30002,#30003,#30004,#30005,#30006));
#7102=EDGE_LOOP('',(#30007,#30008,#30009,#30010,#30011));
#7103=EDGE_LOOP('',(#30012,#30013,#30014,#30015));
#7104=EDGE_LOOP('',(#30016,#30017,#30018,#30019,#30020,#30021));
#7105=EDGE_LOOP('',(#30022,#30023,#30024,#30025,#30026,#30027,#30028));
#7106=EDGE_LOOP('',(#30029,#30030,#30031,#30032,#30033));
#7107=EDGE_LOOP('',(#30034,#30035,#30036,#30037,#30038,#30039));
#7108=EDGE_LOOP('',(#30040,#30041,#30042,#30043,#30044));
#7109=EDGE_LOOP('',(#30045,#30046,#30047,#30048,#30049,#30050));
#7110=EDGE_LOOP('',(#30051,#30052,#30053,#30054,#30055,#30056));
#7111=EDGE_LOOP('',(#30057,#30058,#30059,#30060,#30061));
#7112=EDGE_LOOP('',(#30062,#30063,#30064,#30065));
#7113=EDGE_LOOP('',(#30066,#30067,#30068,#30069,#30070,#30071,#30072,#30073));
#7114=EDGE_LOOP('',(#30074,#30075,#30076,#30077,#30078,#30079,#30080));
#7115=EDGE_LOOP('',(#30081,#30082,#30083,#30084,#30085));
#7116=EDGE_LOOP('',(#30086,#30087,#30088,#30089,#30090,#30091,#30092,#30093));
#7117=EDGE_LOOP('',(#30094,#30095,#30096,#30097,#30098,#30099));
#7118=EDGE_LOOP('',(#30100,#30101,#30102,#30103));
#7119=EDGE_LOOP('',(#30104,#30105,#30106,#30107,#30108,#30109,#30110));
#7120=EDGE_LOOP('',(#30111,#30112,#30113,#30114));
#7121=EDGE_LOOP('',(#30115,#30116,#30117,#30118,#30119,#30120,#30121));
#7122=EDGE_LOOP('',(#30122,#30123,#30124,#30125,#30126));
#7123=EDGE_LOOP('',(#30127,#30128,#30129,#30130,#30131));
#7124=EDGE_LOOP('',(#30132,#30133,#30134,#30135));
#7125=EDGE_LOOP('',(#30136,#30137,#30138));
#7126=EDGE_LOOP('',(#30139,#30140,#30141,#30142));
#7127=EDGE_LOOP('',(#30143,#30144,#30145,#30146));
#7128=EDGE_LOOP('',(#30147,#30148,#30149,#30150,#30151));
#7129=EDGE_LOOP('',(#30152,#30153,#30154,#30155,#30156));
#7130=EDGE_LOOP('',(#30157,#30158,#30159,#30160,#30161));
#7131=EDGE_LOOP('',(#30162,#30163,#30164,#30165,#30166));
#7132=EDGE_LOOP('',(#30167,#30168,#30169,#30170,#30171));
#7133=EDGE_LOOP('',(#30172,#30173,#30174,#30175,#30176));
#7134=EDGE_LOOP('',(#30177,#30178,#30179,#30180,#30181,#30182));
#7135=EDGE_LOOP('',(#30183,#30184,#30185,#30186,#30187,#30188));
#7136=EDGE_LOOP('',(#30189,#30190,#30191,#30192,#30193));
#7137=EDGE_LOOP('',(#30194,#30195,#30196,#30197,#30198,#30199));
#7138=EDGE_LOOP('',(#30200,#30201,#30202,#30203,#30204,#30205));
#7139=EDGE_LOOP('',(#30206,#30207,#30208,#30209,#30210));
#7140=EDGE_LOOP('',(#30211,#30212,#30213,#30214,#30215,#30216,#30217,#30218,
#30219,#30220,#30221,#30222,#30223,#30224,#30225,#30226,#30227,#30228,#30229,
#30230,#30231,#30232,#30233,#30234,#30235,#30236,#30237,#30238,#30239));
#7141=EDGE_LOOP('',(#30240,#30241,#30242,#30243,#30244));
#7142=EDGE_LOOP('',(#30245,#30246,#30247,#30248,#30249));
#7143=EDGE_LOOP('',(#30250,#30251,#30252,#30253));
#7144=EDGE_LOOP('',(#30254,#30255,#30256,#30257,#30258));
#7145=EDGE_LOOP('',(#30259,#30260,#30261,#30262,#30263,#30264,#30265,#30266));
#7146=EDGE_LOOP('',(#30267,#30268,#30269,#30270,#30271,#30272,#30273,#30274));
#7147=EDGE_LOOP('',(#30275,#30276,#30277));
#7148=EDGE_LOOP('',(#30278,#30279,#30280));
#7149=EDGE_LOOP('',(#30281,#30282,#30283,#30284));
#7150=EDGE_LOOP('',(#30285,#30286,#30287));
#7151=EDGE_LOOP('',(#30288,#30289,#30290,#30291));
#7152=EDGE_LOOP('',(#30292,#30293,#30294,#30295));
#7153=EDGE_LOOP('',(#30296,#30297,#30298,#30299,#30300,#30301));
#7154=EDGE_LOOP('',(#30302,#30303,#30304,#30305));
#7155=EDGE_LOOP('',(#30306,#30307,#30308,#30309));
#7156=EDGE_LOOP('',(#30310,#30311,#30312,#30313));
#7157=EDGE_LOOP('',(#30314,#30315,#30316,#30317));
#7158=EDGE_LOOP('',(#30318,#30319,#30320,#30321,#30322,#30323,#30324));
#7159=EDGE_LOOP('',(#30325,#30326,#30327,#30328,#30329,#30330,#30331));
#7160=EDGE_LOOP('',(#30332,#30333,#30334,#30335,#30336));
#7161=EDGE_LOOP('',(#30337,#30338,#30339,#30340));
#7162=EDGE_LOOP('',(#30341,#30342,#30343));
#7163=EDGE_LOOP('',(#30344,#30345,#30346,#30347,#30348));
#7164=EDGE_LOOP('',(#30349,#30350,#30351,#30352));
#7165=EDGE_LOOP('',(#30353,#30354,#30355,#30356,#30357));
#7166=EDGE_LOOP('',(#30358,#30359,#30360,#30361));
#7167=EDGE_LOOP('',(#30362,#30363,#30364,#30365,#30366,#30367,#30368,#30369));
#7168=EDGE_LOOP('',(#30370,#30371,#30372,#30373,#30374));
#7169=EDGE_LOOP('',(#30375,#30376,#30377,#30378,#30379,#30380,#30381));
#7170=EDGE_LOOP('',(#30382,#30383,#30384,#30385,#30386,#30387,#30388));
#7171=EDGE_LOOP('',(#30389,#30390,#30391,#30392,#30393));
#7172=EDGE_LOOP('',(#30394,#30395,#30396,#30397));
#7173=EDGE_LOOP('',(#30398,#30399,#30400,#30401));
#7174=EDGE_LOOP('',(#30402,#30403,#30404,#30405,#30406,#30407,#30408));
#7175=EDGE_LOOP('',(#30409,#30410,#30411,#30412,#30413));
#7176=EDGE_LOOP('',(#30414,#30415,#30416,#30417,#30418,#30419,#30420));
#7177=EDGE_LOOP('',(#30421,#30422,#30423,#30424,#30425,#30426,#30427,#30428,
#30429));
#7178=EDGE_LOOP('',(#30430));
#7179=EDGE_LOOP('',(#30431));
#9982=LINE('',#61986,#13032);
#9983=LINE('',#61992,#13033);
#9984=LINE('',#61993,#13034);
#9985=LINE('',#61998,#13035);
#9986=LINE('',#62026,#13036);
#9987=LINE('',#62032,#13037);
#9988=LINE('',#62034,#13038);
#9989=LINE('',#62035,#13039);
#9990=LINE('',#62038,#13040);
#9991=LINE('',#62039,#13041);
#9992=LINE('',#62042,#13042);
#9993=LINE('',#62044,#13043);
#9994=LINE('',#62045,#13044);
#9995=LINE('',#62048,#13045);
#9996=LINE('',#62050,#13046);
#9997=LINE('',#62052,#13047);
#9998=LINE('',#62054,#13048);
#9999=LINE('',#62055,#13049);
#10000=LINE('',#62058,#13050);
#10001=LINE('',#62064,#13051);
#10002=LINE('',#62065,#13052);
#10003=LINE('',#62068,#13053);
#10004=LINE('',#62070,#13054);
#10005=LINE('',#62074,#13055);
#10006=LINE('',#62076,#13056);
#10007=LINE('',#62078,#13057);
#10008=LINE('',#62079,#13058);
#10009=LINE('',#62085,#13059);
#10010=LINE('',#62101,#13060);
#10011=LINE('',#62103,#13061);
#10012=LINE('',#62109,#13062);
#10013=LINE('',#62110,#13063);
#10014=LINE('',#62113,#13064);
#10015=LINE('',#62115,#13065);
#10016=LINE('',#62121,#13066);
#10017=LINE('',#62123,#13067);
#10018=LINE('',#62125,#13068);
#10019=LINE('',#62131,#13069);
#10020=LINE('',#62133,#13070);
#10021=LINE('',#62135,#13071);
#10022=LINE('',#62136,#13072);
#10023=LINE('',#62138,#13073);
#10024=LINE('',#62139,#13074);
#10025=LINE('',#62147,#13075);
#10026=LINE('',#62153,#13076);
#10027=LINE('',#62154,#13077);
#10028=LINE('',#62176,#13078);
#10029=LINE('',#62202,#13079);
#10030=LINE('',#62203,#13080);
#10031=LINE('',#62206,#13081);
#10032=LINE('',#62211,#13082);
#10033=LINE('',#62218,#13083);
#10034=LINE('',#62220,#13084);
#10035=LINE('',#62221,#13085);
#10036=LINE('',#62226,#13086);
#10037=LINE('',#62267,#13087);
#10038=LINE('',#62273,#13088);
#10039=LINE('',#62274,#13089);
#10040=LINE('',#62279,#13090);
#10041=LINE('',#62307,#13091);
#10042=LINE('',#62313,#13092);
#10043=LINE('',#62315,#13093);
#10044=LINE('',#62316,#13094);
#10045=LINE('',#62319,#13095);
#10046=LINE('',#62320,#13096);
#10047=LINE('',#62323,#13097);
#10048=LINE('',#62325,#13098);
#10049=LINE('',#62326,#13099);
#10050=LINE('',#62328,#13100);
#10051=LINE('',#62329,#13101);
#10052=LINE('',#62332,#13102);
#10053=LINE('',#62333,#13103);
#10054=LINE('',#62336,#13104);
#10055=LINE('',#62337,#13105);
#10056=LINE('',#62339,#13106);
#10057=LINE('',#62342,#13107);
#10058=LINE('',#62344,#13108);
#10059=LINE('',#62345,#13109);
#10060=LINE('',#62348,#13110);
#10061=LINE('',#62349,#13111);
#10062=LINE('',#62352,#13112);
#10063=LINE('',#62353,#13113);
#10064=LINE('',#62356,#13114);
#10065=LINE('',#62358,#13115);
#10066=LINE('',#62360,#13116);
#10067=LINE('',#62361,#13117);
#10068=LINE('',#62364,#13118);
#10069=LINE('',#62370,#13119);
#10070=LINE('',#62371,#13120);
#10071=LINE('',#62374,#13121);
#10072=LINE('',#62376,#13122);
#10073=LINE('',#62380,#13123);
#10074=LINE('',#62382,#13124);
#10075=LINE('',#62384,#13125);
#10076=LINE('',#62385,#13126);
#10077=LINE('',#62391,#13127);
#10078=LINE('',#62406,#13128);
#10079=LINE('',#62408,#13129);
#10080=LINE('',#62410,#13130);
#10081=LINE('',#62412,#13131);
#10082=LINE('',#62413,#13132);
#10083=LINE('',#62416,#13133);
#10084=LINE('',#62417,#13134);
#10085=LINE('',#62420,#13135);
#10086=LINE('',#62448,#13136);
#10087=LINE('',#62454,#13137);
#10088=LINE('',#62455,#13138);
#10089=LINE('',#62460,#13139);
#10090=LINE('',#62462,#13140);
#10091=LINE('',#62468,#13141);
#10092=LINE('',#62470,#13142);
#10093=LINE('',#62471,#13143);
#10094=LINE('',#62474,#13144);
#10095=LINE('',#62476,#13145);
#10096=LINE('',#62477,#13146);
#10097=LINE('',#62483,#13147);
#10098=LINE('',#62486,#13148);
#10099=LINE('',#62492,#13149);
#10100=LINE('',#62494,#13150);
#10101=LINE('',#62499,#13151);
#10102=LINE('',#62502,#13152);
#10103=LINE('',#62504,#13153);
#10104=LINE('',#62509,#13154);
#10105=LINE('',#62512,#13155);
#10106=LINE('',#62517,#13156);
#10107=LINE('',#62531,#13157);
#10108=LINE('',#62533,#13158);
#10109=LINE('',#62534,#13159);
#10110=LINE('',#62538,#13160);
#10111=LINE('',#62545,#13161);
#10112=LINE('',#62556,#13162);
#10113=LINE('',#62559,#13163);
#10114=LINE('',#62565,#13164);
#10115=LINE('',#62568,#13165);
#10116=LINE('',#62579,#13166);
#10117=LINE('',#62583,#13167);
#10118=LINE('',#62585,#13168);
#10119=LINE('',#62591,#13169);
#10120=LINE('',#62610,#13170);
#10121=LINE('',#62616,#13171);
#10122=LINE('',#62626,#13172);
#10123=LINE('',#62635,#13173);
#10124=LINE('',#62639,#13174);
#10125=LINE('',#62643,#13175);
#10126=LINE('',#62647,#13176);
#10127=LINE('',#62665,#13177);
#10128=LINE('',#62670,#13178);
#10129=LINE('',#62673,#13179);
#10130=LINE('',#62678,#13180);
#10131=LINE('',#62680,#13181);
#10132=LINE('',#62704,#13182);
#10133=LINE('',#62706,#13183);
#10134=LINE('',#62707,#13184);
#10135=LINE('',#62709,#13185);
#10136=LINE('',#62714,#13186);
#10137=LINE('',#62721,#13187);
#10138=LINE('',#62722,#13188);
#10139=LINE('',#62725,#13189);
#10140=LINE('',#62732,#13190);
#10141=LINE('',#62733,#13191);
#10142=LINE('',#62735,#13192);
#10143=LINE('',#62736,#13193);
#10144=LINE('',#62739,#13194);
#10145=LINE('',#62760,#13195);
#10146=LINE('',#62761,#13196);
#10147=LINE('',#62769,#13197);
#10148=LINE('',#62785,#13198);
#10149=LINE('',#62786,#13199);
#10150=LINE('',#62788,#13200);
#10151=LINE('',#62790,#13201);
#10152=LINE('',#62791,#13202);
#10153=LINE('',#62794,#13203);
#10154=LINE('',#62795,#13204);
#10155=LINE('',#62798,#13205);
#10156=LINE('',#62799,#13206);
#10157=LINE('',#62802,#13207);
#10158=LINE('',#62803,#13208);
#10159=LINE('',#62813,#13209);
#10160=LINE('',#62815,#13210);
#10161=LINE('',#62817,#13211);
#10162=LINE('',#62822,#13212);
#13032=VECTOR('',#45457,10.);
#13033=VECTOR('',#45458,10.);
#13034=VECTOR('',#45459,10.);
#13035=VECTOR('',#45464,10.);
#13036=VECTOR('',#45471,10.);
#13037=VECTOR('',#45472,10.);
#13038=VECTOR('',#45473,10.);
#13039=VECTOR('',#45474,10.);
#13040=VECTOR('',#45477,10.);
#13041=VECTOR('',#45478,10.);
#13042=VECTOR('',#45481,10.);
#13043=VECTOR('',#45482,10.);
#13044=VECTOR('',#45483,10.);
#13045=VECTOR('',#45486,10.);
#13046=VECTOR('',#45487,10.);
#13047=VECTOR('',#45488,10.);
#13048=VECTOR('',#45489,10.);
#13049=VECTOR('',#45490,10.);
#13050=VECTOR('',#45493,10.);
#13051=VECTOR('',#45494,10.);
#13052=VECTOR('',#45495,10.);
#13053=VECTOR('',#45498,10.);
#13054=VECTOR('',#45499,10.);
#13055=VECTOR('',#45504,10.);
#13056=VECTOR('',#45505,10.);
#13057=VECTOR('',#45506,10.);
#13058=VECTOR('',#45507,10.);
#13059=VECTOR('',#45510,10.);
#13060=VECTOR('',#45517,10.);
#13061=VECTOR('',#45518,10.);
#13062=VECTOR('',#45519,10.);
#13063=VECTOR('',#45520,10.);
#13064=VECTOR('',#45523,10.);
#13065=VECTOR('',#45524,10.);
#13066=VECTOR('',#45525,10.);
#13067=VECTOR('',#45526,10.);
#13068=VECTOR('',#45527,10.);
#13069=VECTOR('',#45530,10.);
#13070=VECTOR('',#45531,10.);
#13071=VECTOR('',#45532,10.);
#13072=VECTOR('',#45533,10.);
#13073=VECTOR('',#45536,10.);
#13074=VECTOR('',#45537,10.);
#13075=VECTOR('',#45540,10.);
#13076=VECTOR('',#45541,10.);
#13077=VECTOR('',#45542,10.);
#13078=VECTOR('',#45553,10.);
#13079=VECTOR('',#45558,10.);
#13080=VECTOR('',#45559,10.);
#13081=VECTOR('',#45562,10.);
#13082=VECTOR('',#45563,10.);
#13083=VECTOR('',#45566,10.);
#13084=VECTOR('',#45567,10.);
#13085=VECTOR('',#45568,10.);
#13086=VECTOR('',#45573,19.8);
#13087=VECTOR('',#45576,10.);
#13088=VECTOR('',#45577,10.);
#13089=VECTOR('',#45578,10.);
#13090=VECTOR('',#45583,10.);
#13091=VECTOR('',#45590,10.);
#13092=VECTOR('',#45591,10.);
#13093=VECTOR('',#45592,10.);
#13094=VECTOR('',#45593,10.);
#13095=VECTOR('',#45596,10.);
#13096=VECTOR('',#45597,10.);
#13097=VECTOR('',#45600,10.);
#13098=VECTOR('',#45601,10.);
#13099=VECTOR('',#45602,10.);
#13100=VECTOR('',#45605,10.);
#13101=VECTOR('',#45606,10.);
#13102=VECTOR('',#45609,10.);
#13103=VECTOR('',#45610,10.);
#13104=VECTOR('',#45613,10.);
#13105=VECTOR('',#45614,10.);
#13106=VECTOR('',#45617,10.);
#13107=VECTOR('',#45620,10.);
#13108=VECTOR('',#45621,10.);
#13109=VECTOR('',#45622,10.);
#13110=VECTOR('',#45625,10.);
#13111=VECTOR('',#45626,10.);
#13112=VECTOR('',#45629,10.);
#13113=VECTOR('',#45630,10.);
#13114=VECTOR('',#45633,10.);
#13115=VECTOR('',#45634,10.);
#13116=VECTOR('',#45635,10.);
#13117=VECTOR('',#45636,10.);
#13118=VECTOR('',#45639,10.);
#13119=VECTOR('',#45640,10.);
#13120=VECTOR('',#45641,10.);
#13121=VECTOR('',#45644,10.);
#13122=VECTOR('',#45645,10.);
#13123=VECTOR('',#45650,10.);
#13124=VECTOR('',#45651,10.);
#13125=VECTOR('',#45652,10.);
#13126=VECTOR('',#45653,10.);
#13127=VECTOR('',#45656,10.);
#13128=VECTOR('',#45663,10.);
#13129=VECTOR('',#45664,10.);
#13130=VECTOR('',#45665,10.);
#13131=VECTOR('',#45666,10.);
#13132=VECTOR('',#45667,10.);
#13133=VECTOR('',#45670,10.);
#13134=VECTOR('',#45671,10.);
#13135=VECTOR('',#45674,10.);
#13136=VECTOR('',#45681,10.);
#13137=VECTOR('',#45682,10.);
#13138=VECTOR('',#45683,10.);
#13139=VECTOR('',#45690,10.);
#13140=VECTOR('',#45691,10.);
#13141=VECTOR('',#45692,10.);
#13142=VECTOR('',#45693,10.);
#13143=VECTOR('',#45694,10.);
#13144=VECTOR('',#45697,10.);
#13145=VECTOR('',#45698,10.);
#13146=VECTOR('',#45699,10.);
#13147=VECTOR('',#45702,10.);
#13148=VECTOR('',#45705,10.);
#13149=VECTOR('',#45706,10.);
#13150=VECTOR('',#45707,10.);
#13151=VECTOR('',#45710,10.);
#13152=VECTOR('',#45713,10.);
#13153=VECTOR('',#45714,10.);
#13154=VECTOR('',#45715,10.);
#13155=VECTOR('',#45718,10.);
#13156=VECTOR('',#45719,10.);
#13157=VECTOR('',#45728,10.);
#13158=VECTOR('',#45731,10.);
#13159=VECTOR('',#45732,10.);
#13160=VECTOR('',#45737,10.);
#13161=VECTOR('',#45740,10.);
#13162=VECTOR('',#45743,10.);
#13163=VECTOR('',#45746,10.);
#13164=VECTOR('',#45747,10.);
#13165=VECTOR('',#45750,10.);
#13166=VECTOR('',#45753,10.);
#13167=VECTOR('',#45756,10.);
#13168=VECTOR('',#45757,10.);
#13169=VECTOR('',#45758,10.);
#13170=VECTOR('',#45771,10.);
#13171=VECTOR('',#45772,10.);
#13172=VECTOR('',#45783,10.);
#13173=VECTOR('',#45788,10.);
#13174=VECTOR('',#45791,10.);
#13175=VECTOR('',#45794,10.);
#13176=VECTOR('',#45797,12.75);
#13177=VECTOR('',#45810,10.);
#13178=VECTOR('',#45811,10.);
#13179=VECTOR('',#45814,10.);
#13180=VECTOR('',#45815,10.);
#13181=VECTOR('',#45818,10.);
#13182=VECTOR('',#45825,10.);
#13183=VECTOR('',#45826,10.);
#13184=VECTOR('',#45827,10.);
#13185=VECTOR('',#45830,10.);
#13186=VECTOR('',#45831,10.);
#13187=VECTOR('',#45834,10.);
#13188=VECTOR('',#45835,10.);
#13189=VECTOR('',#45838,10.);
#13190=VECTOR('',#45841,10.);
#13191=VECTOR('',#45842,10.);
#13192=VECTOR('',#45845,10.);
#13193=VECTOR('',#45846,10.);
#13194=VECTOR('',#45849,10.);
#13195=VECTOR('',#45856,10.);
#13196=VECTOR('',#45857,10.);
#13197=VECTOR('',#45864,10.);
#13198=VECTOR('',#45877,10.);
#13199=VECTOR('',#45878,10.);
#13200=VECTOR('',#45881,10.);
#13201=VECTOR('',#45882,10.);
#13202=VECTOR('',#45883,10.);
#13203=VECTOR('',#45886,10.);
#13204=VECTOR('',#45887,10.);
#13205=VECTOR('',#45890,10.);
#13206=VECTOR('',#45891,10.);
#13207=VECTOR('',#45894,10.);
#13208=VECTOR('',#45895,10.);
#13209=VECTOR('',#45906,13.075);
#13210=VECTOR('',#45909,10.);
#13211=VECTOR('',#45912,10.);
#13212=VECTOR('',#45921,10.);
#14350=CIRCLE('',#37040,17.8588235294118);
#14351=CIRCLE('',#37041,13.25);
#14352=CIRCLE('',#37049,13.25);
#14353=CIRCLE('',#37053,12.75);
#14354=CIRCLE('',#37060,13.25);
#14355=CIRCLE('',#37061,12.75);
#14356=CIRCLE('',#37063,17.8588235294118);
#14357=CIRCLE('',#37069,17.8588235294118);
#14358=CIRCLE('',#37072,17.8588235294118);
#14359=CIRCLE('',#37073,13.25);
#14360=CIRCLE('',#37088,13.25);
#14361=CIRCLE('',#37092,12.75);
#14362=CIRCLE('',#37097,17.8588235294118);
#14363=CIRCLE('',#37100,13.25);
#14364=CIRCLE('',#37109,13.25);
#14365=CIRCLE('',#37110,12.75);
#14366=CIRCLE('',#37122,12.75);
#14367=CIRCLE('',#37124,13.25);
#14368=CIRCLE('',#37125,12.75);
#14369=CIRCLE('',#37128,12.75);
#14370=CIRCLE('',#37130,12.75);
#14371=CIRCLE('',#37133,12.75);
#14372=CIRCLE('',#37134,12.75);
#14373=CIRCLE('',#37135,12.75);
#14374=CIRCLE('',#37136,12.75);
#14375=CIRCLE('',#37137,12.75);
#14376=CIRCLE('',#37138,12.75);
#14377=CIRCLE('',#37139,12.75);
#14378=CIRCLE('',#37141,13.25);
#14379=CIRCLE('',#37146,17.8588235294118);
#14380=CIRCLE('',#37155,13.25);
#14381=CIRCLE('',#37158,13.25);
#14382=CIRCLE('',#37162,13.25);
#14383=CIRCLE('',#37172,17.8588235294118);
#14384=CIRCLE('',#37174,13.3071428571429);
#16767=VERTEX_POINT('',#61980);
#16768=VERTEX_POINT('',#61981);
#16769=VERTEX_POINT('',#61985);
#16770=VERTEX_POINT('',#61987);
#16771=VERTEX_POINT('',#61991);
#16772=VERTEX_POINT('',#61995);
#16773=VERTEX_POINT('',#61997);
#16774=VERTEX_POINT('',#62001);
#16775=VERTEX_POINT('',#62005);
#16776=VERTEX_POINT('',#62009);
#16777=VERTEX_POINT('',#62013);
#16778=VERTEX_POINT('',#62017);
#16779=VERTEX_POINT('',#62025);
#16780=VERTEX_POINT('',#62027);
#16781=VERTEX_POINT('',#62031);
#16782=VERTEX_POINT('',#62033);
#16783=VERTEX_POINT('',#62037);
#16784=VERTEX_POINT('',#62041);
#16785=VERTEX_POINT('',#62043);
#16786=VERTEX_POINT('',#62047);
#16787=VERTEX_POINT('',#62049);
#16788=VERTEX_POINT('',#62051);
#16789=VERTEX_POINT('',#62053);
#16790=VERTEX_POINT('',#62057);
#16791=VERTEX_POINT('',#62059);
#16792=VERTEX_POINT('',#62063);
#16793=VERTEX_POINT('',#62067);
#16794=VERTEX_POINT('',#62069);
#16795=VERTEX_POINT('',#62073);
#16796=VERTEX_POINT('',#62075);
#16797=VERTEX_POINT('',#62077);
#16798=VERTEX_POINT('',#62081);
#16799=VERTEX_POINT('',#62087);
#16800=VERTEX_POINT('',#62092);
#16801=VERTEX_POINT('',#62099);
#16802=VERTEX_POINT('',#62100);
#16803=VERTEX_POINT('',#62102);
#16804=VERTEX_POINT('',#62104);
#16805=VERTEX_POINT('',#62108);
#16806=VERTEX_POINT('',#62112);
#16807=VERTEX_POINT('',#62114);
#16808=VERTEX_POINT('',#62116);
#16809=VERTEX_POINT('',#62120);
#16810=VERTEX_POINT('',#62122);
#16811=VERTEX_POINT('',#62124);
#16812=VERTEX_POINT('',#62130);
#16813=VERTEX_POINT('',#62132);
#16814=VERTEX_POINT('',#62134);
#16815=VERTEX_POINT('',#62141);
#16816=VERTEX_POINT('',#62142);
#16817=VERTEX_POINT('',#62146);
#16818=VERTEX_POINT('',#62148);
#16819=VERTEX_POINT('',#62152);
#16820=VERTEX_POINT('',#62156);
#16821=VERTEX_POINT('',#62158);
#16822=VERTEX_POINT('',#62162);
#16823=VERTEX_POINT('',#62167);
#16824=VERTEX_POINT('',#62174);
#16825=VERTEX_POINT('',#62178);
#16826=VERTEX_POINT('',#62182);
#16827=VERTEX_POINT('',#62186);
#16828=VERTEX_POINT('',#62190);
#16829=VERTEX_POINT('',#62194);
#16830=VERTEX_POINT('',#62205);
#16831=VERTEX_POINT('',#62207);
#16832=VERTEX_POINT('',#62213);
#16833=VERTEX_POINT('',#62217);
#16834=VERTEX_POINT('',#62219);
#16835=VERTEX_POINT('',#62223);
#16836=VERTEX_POINT('',#62225);
#16837=VERTEX_POINT('',#62230);
#16838=VERTEX_POINT('',#62234);
#16839=VERTEX_POINT('',#62238);
#16840=VERTEX_POINT('',#62242);
#16841=VERTEX_POINT('',#62246);
#16842=VERTEX_POINT('',#62250);
#16843=VERTEX_POINT('',#62261);
#16844=VERTEX_POINT('',#62262);
#16845=VERTEX_POINT('',#62266);
#16846=VERTEX_POINT('',#62268);
#16847=VERTEX_POINT('',#62272);
#16848=VERTEX_POINT('',#62276);
#16849=VERTEX_POINT('',#62278);
#16850=VERTEX_POINT('',#62282);
#16851=VERTEX_POINT('',#62286);
#16852=VERTEX_POINT('',#62290);
#16853=VERTEX_POINT('',#62294);
#16854=VERTEX_POINT('',#62298);
#16855=VERTEX_POINT('',#62306);
#16856=VERTEX_POINT('',#62308);
#16857=VERTEX_POINT('',#62312);
#16858=VERTEX_POINT('',#62314);
#16859=VERTEX_POINT('',#62318);
#16860=VERTEX_POINT('',#62322);
#16861=VERTEX_POINT('',#62324);
#16862=VERTEX_POINT('',#62331);
#16863=VERTEX_POINT('',#62335);
#16864=VERTEX_POINT('',#62341);
#16865=VERTEX_POINT('',#62343);
#16866=VERTEX_POINT('',#62347);
#16867=VERTEX_POINT('',#62351);
#16868=VERTEX_POINT('',#62355);
#16869=VERTEX_POINT('',#62357);
#16870=VERTEX_POINT('',#62359);
#16871=VERTEX_POINT('',#62363);
#16872=VERTEX_POINT('',#62365);
#16873=VERTEX_POINT('',#62369);
#16874=VERTEX_POINT('',#62373);
#16875=VERTEX_POINT('',#62375);
#16876=VERTEX_POINT('',#62379);
#16877=VERTEX_POINT('',#62381);
#16878=VERTEX_POINT('',#62383);
#16879=VERTEX_POINT('',#62387);
#16880=VERTEX_POINT('',#62393);
#16881=VERTEX_POINT('',#62398);
#16882=VERTEX_POINT('',#62405);
#16883=VERTEX_POINT('',#62407);
#16884=VERTEX_POINT('',#62409);
#16885=VERTEX_POINT('',#62411);
#16886=VERTEX_POINT('',#62415);
#16887=VERTEX_POINT('',#62419);
#16888=VERTEX_POINT('',#62425);
#16889=VERTEX_POINT('',#62429);
#16890=VERTEX_POINT('',#62433);
#16891=VERTEX_POINT('',#62435);
#16892=VERTEX_POINT('',#62439);
#16893=VERTEX_POINT('',#62447);
#16894=VERTEX_POINT('',#62449);
#16895=VERTEX_POINT('',#62453);
#16896=VERTEX_POINT('',#62459);
#16897=VERTEX_POINT('',#62461);
#16898=VERTEX_POINT('',#62463);
#16899=VERTEX_POINT('',#62467);
#16900=VERTEX_POINT('',#62469);
#16901=VERTEX_POINT('',#62473);
#16902=VERTEX_POINT('',#62475);
#16903=VERTEX_POINT('',#62479);
#16904=VERTEX_POINT('',#62485);
#16905=VERTEX_POINT('',#62487);
#16906=VERTEX_POINT('',#62491);
#16907=VERTEX_POINT('',#62493);
#16908=VERTEX_POINT('',#62501);
#16909=VERTEX_POINT('',#62503);
#16910=VERTEX_POINT('',#62505);
#16911=VERTEX_POINT('',#62511);
#16912=VERTEX_POINT('',#62513);
#16913=VERTEX_POINT('',#62519);
#16914=VERTEX_POINT('',#62521);
#16915=VERTEX_POINT('',#62525);
#16916=VERTEX_POINT('',#62537);
#16917=VERTEX_POINT('',#62544);
#16918=VERTEX_POINT('',#62551);
#16919=VERTEX_POINT('',#62558);
#16920=VERTEX_POINT('',#62560);
#16921=VERTEX_POINT('',#62567);
#16922=VERTEX_POINT('',#62574);
#16923=VERTEX_POINT('',#62581);
#16924=VERTEX_POINT('',#62582);
#16925=VERTEX_POINT('',#62584);
#16926=VERTEX_POINT('',#62586);
#16927=VERTEX_POINT('',#62590);
#16928=VERTEX_POINT('',#62602);
#16929=VERTEX_POINT('',#62609);
#16930=VERTEX_POINT('',#62611);
#16931=VERTEX_POINT('',#62625);
#16932=VERTEX_POINT('',#62632);
#16933=VERTEX_POINT('',#62634);
#16934=VERTEX_POINT('',#62636);
#16935=VERTEX_POINT('',#62638);
#16936=VERTEX_POINT('',#62640);
#16937=VERTEX_POINT('',#62642);
#16938=VERTEX_POINT('',#62644);
#16939=VERTEX_POINT('',#62646);
#16940=VERTEX_POINT('',#62648);
#16941=VERTEX_POINT('',#62653);
#16942=VERTEX_POINT('',#62658);
#16943=VERTEX_POINT('',#62664);
#16944=VERTEX_POINT('',#62666);
#16945=VERTEX_POINT('',#62672);
#16946=VERTEX_POINT('',#62674);
#16947=VERTEX_POINT('',#62682);
#16948=VERTEX_POINT('',#62686);
#16949=VERTEX_POINT('',#62690);
#16950=VERTEX_POINT('',#62694);
#16951=VERTEX_POINT('',#62703);
#16952=VERTEX_POINT('',#62705);
#16953=VERTEX_POINT('',#62710);
#16954=VERTEX_POINT('',#62716);
#16955=VERTEX_POINT('',#62720);
#16956=VERTEX_POINT('',#62724);
#16957=VERTEX_POINT('',#62731);
#16958=VERTEX_POINT('',#62738);
#16959=VERTEX_POINT('',#62745);
#16960=VERTEX_POINT('',#62749);
#16961=VERTEX_POINT('',#62755);
#16962=VERTEX_POINT('',#62756);
#16963=VERTEX_POINT('',#62765);
#16964=VERTEX_POINT('',#62780);
#16965=VERTEX_POINT('',#62784);
#16966=VERTEX_POINT('',#62789);
#16967=VERTEX_POINT('',#62793);
#16968=VERTEX_POINT('',#62797);
#16969=VERTEX_POINT('',#62801);
#16970=VERTEX_POINT('',#62811);
#21215=EDGE_CURVE('',#16767,#16768,#183,.T.);
#21216=EDGE_CURVE('',#16768,#16769,#9982,.T.);
#21217=EDGE_CURVE('',#16769,#16770,#184,.T.);
#21218=EDGE_CURVE('',#16770,#16771,#9983,.T.);
#21219=EDGE_CURVE('',#16771,#16767,#9984,.T.);
#21220=EDGE_CURVE('',#16768,#16772,#14350,.T.);
#21221=EDGE_CURVE('',#16773,#16772,#9985,.T.);
#21222=EDGE_CURVE('',#16769,#16773,#14351,.T.);
#21223=EDGE_CURVE('',#16767,#16774,#185,.T.);
#21224=EDGE_CURVE('',#16775,#16774,#186,.T.);
#21225=EDGE_CURVE('',#16776,#16775,#187,.T.);
#21226=EDGE_CURVE('',#16777,#16776,#188,.T.);
#21227=EDGE_CURVE('',#16777,#16778,#189,.T.);
#21228=EDGE_CURVE('',#16772,#16778,#190,.T.);
#21229=EDGE_CURVE('',#16779,#16771,#9986,.T.);
#21230=EDGE_CURVE('',#16780,#16779,#191,.T.);
#21231=EDGE_CURVE('',#16780,#16781,#9987,.T.);
#21232=EDGE_CURVE('',#16782,#16781,#9988,.F.);
#21233=EDGE_CURVE('',#16774,#16782,#9989,.T.);
#21234=EDGE_CURVE('',#16782,#16783,#9990,.F.);
#21235=EDGE_CURVE('',#16783,#16775,#9991,.T.);
#21236=EDGE_CURVE('',#16784,#16777,#9992,.T.);
#21237=EDGE_CURVE('',#16776,#16785,#9993,.T.);
#21238=EDGE_CURVE('',#16785,#16784,#9994,.T.);
#21239=EDGE_CURVE('',#16785,#16786,#9995,.T.);
#21240=EDGE_CURVE('',#16786,#16787,#9996,.T.);
#21241=EDGE_CURVE('',#16787,#16788,#9997,.T.);
#21242=EDGE_CURVE('',#16788,#16789,#9998,.T.);
#21243=EDGE_CURVE('',#16789,#16784,#9999,.T.);
#21244=EDGE_CURVE('',#16789,#16790,#10000,.T.);
#21245=EDGE_CURVE('',#16791,#16790,#192,.T.);
#21246=EDGE_CURVE('',#16792,#16791,#10001,.T.);
#21247=EDGE_CURVE('',#16778,#16792,#10002,.T.);
#21248=EDGE_CURVE('',#16793,#16788,#10003,.T.);
#21249=EDGE_CURVE('',#16794,#16793,#10004,.T.);
#21250=EDGE_CURVE('',#16790,#16794,#14352,.T.);
#21251=EDGE_CURVE('',#16787,#16795,#10005,.T.);
#21252=EDGE_CURVE('',#16795,#16796,#10006,.T.);
#21253=EDGE_CURVE('',#16797,#16796,#10007,.T.);
#21254=EDGE_CURVE('',#16797,#16793,#10008,.T.);
#21255=EDGE_CURVE('',#16798,#16773,#193,.T.);
#21256=EDGE_CURVE('',#16792,#16798,#10009,.T.);
#21257=EDGE_CURVE('',#16798,#16799,#655,.T.);
#21258=EDGE_CURVE('',#16799,#16800,#14353,.T.);
#21259=EDGE_CURVE('',#16770,#16800,#656,.T.);
#21260=EDGE_CURVE('',#16801,#16802,#10010,.T.);
#21261=EDGE_CURVE('',#16802,#16803,#10011,.T.);
#21262=EDGE_CURVE('',#16803,#16804,#194,.T.);
#21263=EDGE_CURVE('',#16804,#16805,#10012,.T.);
#21264=EDGE_CURVE('',#16805,#16801,#10013,.T.);
#21265=EDGE_CURVE('',#16806,#16802,#10014,.T.);
#21266=EDGE_CURVE('',#16807,#16806,#10015,.T.);
#21267=EDGE_CURVE('',#16807,#16808,#195,.T.);
#21268=EDGE_CURVE('',#16809,#16808,#10016,.T.);
#21269=EDGE_CURVE('',#16810,#16809,#10017,.T.);
#21270=EDGE_CURVE('',#16811,#16810,#10018,.T.);
#21271=EDGE_CURVE('',#16811,#16803,#196,.T.);
#21272=EDGE_CURVE('',#16812,#16801,#10019,.T.);
#21273=EDGE_CURVE('',#16812,#16813,#10020,.T.);
#21274=EDGE_CURVE('',#16813,#16814,#10021,.T.);
#21275=EDGE_CURVE('',#16806,#16814,#10022,.T.);
#21276=EDGE_CURVE('',#16805,#16783,#10023,.T.);
#21277=EDGE_CURVE('',#16781,#16812,#10024,.T.);
#21278=EDGE_CURVE('',#16815,#16816,#197,.T.);
#21279=EDGE_CURVE('',#16816,#16817,#10025,.T.);
#21280=EDGE_CURVE('',#16817,#16818,#198,.T.);
#21281=EDGE_CURVE('',#16818,#16819,#10026,.T.);
#21282=EDGE_CURVE('',#16819,#16815,#10027,.T.);
#21283=EDGE_CURVE('',#16817,#16820,#14354,.T.);
#21284=EDGE_CURVE('',#16821,#16820,#199,.T.);
#21285=EDGE_CURVE('',#16821,#16822,#657,.T.);
#21286=EDGE_CURVE('',#16822,#16823,#14355,.T.);
#21287=EDGE_CURVE('',#16823,#16818,#658,.T.);
#21288=EDGE_CURVE('',#16816,#16824,#14356,.T.);
#21289=EDGE_CURVE('',#16820,#16824,#10028,.T.);
#21290=EDGE_CURVE('',#16815,#16825,#200,.T.);
#21291=EDGE_CURVE('',#16826,#16825,#201,.T.);
#21292=EDGE_CURVE('',#16827,#16826,#202,.T.);
#21293=EDGE_CURVE('',#16828,#16827,#203,.T.);
#21294=EDGE_CURVE('',#16828,#16829,#204,.T.);
#21295=EDGE_CURVE('',#16824,#16829,#205,.T.);
#21296=EDGE_CURVE('',#16796,#16826,#10029,.T.);
#21297=EDGE_CURVE('',#16825,#16797,#10030,.T.);
#21298=EDGE_CURVE('',#16786,#16830,#10031,.T.);
#21299=EDGE_CURVE('',#16830,#16831,#206,.T.);
#21300=EDGE_CURVE('',#16831,#16795,#10032,.T.);
#21301=EDGE_CURVE('',#16831,#16832,#207,.T.);
#21302=EDGE_CURVE('',#16833,#16832,#10033,.T.);
#21303=EDGE_CURVE('',#16834,#16833,#10034,.T.);
#21304=EDGE_CURVE('',#16827,#16834,#10035,.T.);
#21305=EDGE_CURVE('',#16835,#16835,#14357,.T.);
#21306=EDGE_CURVE('',#16835,#16836,#10036,.T.);
#21307=EDGE_CURVE('',#16804,#16836,#208,.T.);
#21308=EDGE_CURVE('',#16837,#16811,#209,.T.);
#21309=EDGE_CURVE('',#16838,#16837,#210,.T.);
#21310=EDGE_CURVE('',#16839,#16838,#211,.T.);
#21311=EDGE_CURVE('',#16840,#16839,#212,.T.);
#21312=EDGE_CURVE('',#16841,#16840,#213,.T.);
#21313=EDGE_CURVE('',#16842,#16841,#214,.T.);
#21314=EDGE_CURVE('',#16832,#16842,#215,.T.);
#21315=EDGE_CURVE('',#16836,#16830,#216,.T.);
#21316=EDGE_CURVE('',#16843,#16844,#217,.T.);
#21317=EDGE_CURVE('',#16844,#16845,#10037,.T.);
#21318=EDGE_CURVE('',#16845,#16846,#218,.T.);
#21319=EDGE_CURVE('',#16846,#16847,#10038,.T.);
#21320=EDGE_CURVE('',#16847,#16843,#10039,.T.);
#21321=EDGE_CURVE('',#16844,#16848,#14358,.T.);
#21322=EDGE_CURVE('',#16849,#16848,#10040,.T.);
#21323=EDGE_CURVE('',#16845,#16849,#14359,.T.);
#21324=EDGE_CURVE('',#16843,#16850,#219,.T.);
#21325=EDGE_CURVE('',#16851,#16850,#220,.T.);
#21326=EDGE_CURVE('',#16852,#16851,#221,.T.);
#21327=EDGE_CURVE('',#16853,#16852,#222,.T.);
#21328=EDGE_CURVE('',#16853,#16854,#223,.T.);
#21329=EDGE_CURVE('',#16848,#16854,#224,.T.);
#21330=EDGE_CURVE('',#16855,#16847,#10041,.T.);
#21331=EDGE_CURVE('',#16856,#16855,#225,.T.);
#21332=EDGE_CURVE('',#16856,#16857,#10042,.T.);
#21333=EDGE_CURVE('',#16858,#16857,#10043,.T.);
#21334=EDGE_CURVE('',#16850,#16858,#10044,.T.);
#21335=EDGE_CURVE('',#16859,#16851,#10045,.T.);
#21336=EDGE_CURVE('',#16858,#16859,#10046,.T.);
#21337=EDGE_CURVE('',#16860,#16833,#10047,.T.);
#21338=EDGE_CURVE('',#16861,#16860,#10048,.T.);
#21339=EDGE_CURVE('',#16833,#16861,#10049,.T.);
#21340=EDGE_CURVE('',#16857,#16861,#10050,.T.);
#21341=EDGE_CURVE('',#16860,#16859,#10051,.T.);
#21342=EDGE_CURVE('',#16862,#16828,#10052,.T.);
#21343=EDGE_CURVE('',#16834,#16862,#10053,.T.);
#21344=EDGE_CURVE('',#16861,#16863,#10054,.T.);
#21345=EDGE_CURVE('',#16863,#16862,#10055,.T.);
#21346=EDGE_CURVE('',#16842,#16860,#10056,.T.);
#21347=EDGE_CURVE('',#16864,#16841,#10057,.T.);
#21348=EDGE_CURVE('',#16865,#16864,#10058,.T.);
#21349=EDGE_CURVE('',#16852,#16865,#10059,.T.);
#21350=EDGE_CURVE('',#16829,#16866,#10060,.T.);
#21351=EDGE_CURVE('',#16866,#16821,#10061,.T.);
#21352=EDGE_CURVE('',#16867,#16853,#10062,.T.);
#21353=EDGE_CURVE('',#16865,#16867,#10063,.T.);
#21354=EDGE_CURVE('',#16864,#16868,#10064,.T.);
#21355=EDGE_CURVE('',#16868,#16869,#10065,.T.);
#21356=EDGE_CURVE('',#16869,#16870,#10066,.T.);
#21357=EDGE_CURVE('',#16870,#16867,#10067,.T.);
#21358=EDGE_CURVE('',#16870,#16871,#10068,.T.);
#21359=EDGE_CURVE('',#16872,#16871,#226,.T.);
#21360=EDGE_CURVE('',#16873,#16872,#10069,.T.);
#21361=EDGE_CURVE('',#16854,#16873,#10070,.T.);
#21362=EDGE_CURVE('',#16874,#16869,#10071,.T.);
#21363=EDGE_CURVE('',#16875,#16874,#10072,.T.);
#21364=EDGE_CURVE('',#16871,#16875,#14360,.T.);
#21365=EDGE_CURVE('',#16868,#16876,#10073,.T.);
#21366=EDGE_CURVE('',#16876,#16877,#10074,.T.);
#21367=EDGE_CURVE('',#16878,#16877,#10075,.T.);
#21368=EDGE_CURVE('',#16878,#16874,#10076,.T.);
#21369=EDGE_CURVE('',#16879,#16849,#227,.T.);
#21370=EDGE_CURVE('',#16873,#16879,#10077,.T.);
#21371=EDGE_CURVE('',#16879,#16880,#659,.T.);
#21372=EDGE_CURVE('',#16880,#16881,#14361,.T.);
#21373=EDGE_CURVE('',#16846,#16881,#660,.T.);
#21374=EDGE_CURVE('',#16882,#16810,#10078,.T.);
#21375=EDGE_CURVE('',#16809,#16883,#10079,.F.);
#21376=EDGE_CURVE('',#16883,#16884,#10080,.F.);
#21377=EDGE_CURVE('',#16884,#16885,#10081,.T.);
#21378=EDGE_CURVE('',#16885,#16882,#10082,.T.);
#21379=EDGE_CURVE('',#16882,#16886,#10083,.T.);
#21380=EDGE_CURVE('',#16886,#16837,#10084,.T.);
#21381=EDGE_CURVE('',#16814,#16887,#10085,.T.);
#21382=EDGE_CURVE('',#16887,#16807,#228,.T.);
#21383=EDGE_CURVE('',#16887,#16888,#229,.T.);
#21384=EDGE_CURVE('',#16889,#16888,#230,.T.);
#21385=EDGE_CURVE('',#16890,#16889,#14362,.T.);
#21386=EDGE_CURVE('',#16891,#16890,#231,.T.);
#21387=EDGE_CURVE('',#16891,#16892,#232,.T.);
#21388=EDGE_CURVE('',#16808,#16892,#233,.T.);
#21389=EDGE_CURVE('',#16813,#16893,#10086,.T.);
#21390=EDGE_CURVE('',#16894,#16893,#234,.T.);
#21391=EDGE_CURVE('',#16895,#16894,#10087,.T.);
#21392=EDGE_CURVE('',#16888,#16895,#10088,.T.);
#21393=EDGE_CURVE('',#16893,#16780,#14363,.T.);
#21394=EDGE_CURVE('',#16896,#16886,#10089,.T.);
#21395=EDGE_CURVE('',#16897,#16896,#10090,.T.);
#21396=EDGE_CURVE('',#16897,#16898,#235,.T.);
#21397=EDGE_CURVE('',#16899,#16898,#10091,.T.);
#21398=EDGE_CURVE('',#16900,#16899,#10092,.T.);
#21399=EDGE_CURVE('',#16838,#16900,#10093,.T.);
#21400=EDGE_CURVE('',#16885,#16901,#10094,.T.);
#21401=EDGE_CURVE('',#16901,#16902,#10095,.F.);
#21402=EDGE_CURVE('',#16896,#16902,#10096,.F.);
#21403=EDGE_CURVE('',#16903,#16897,#236,.T.);
#21404=EDGE_CURVE('',#16902,#16903,#10097,.T.);
#21405=EDGE_CURVE('',#16901,#16904,#10098,.T.);
#21406=EDGE_CURVE('',#16905,#16904,#237,.T.);
#21407=EDGE_CURVE('',#16906,#16905,#10099,.T.);
#21408=EDGE_CURVE('',#16907,#16906,#10100,.T.);
#21409=EDGE_CURVE('',#16903,#16907,#238,.T.);
#21410=EDGE_CURVE('',#16892,#16883,#10101,.T.);
#21411=EDGE_CURVE('',#16908,#16891,#10102,.T.);
#21412=EDGE_CURVE('',#16909,#16908,#10103,.T.);
#21413=EDGE_CURVE('',#16910,#16909,#239,.T.);
#21414=EDGE_CURVE('',#16910,#16884,#10104,.T.);
#21415=EDGE_CURVE('',#16890,#16911,#10105,.T.);
#21416=EDGE_CURVE('',#16911,#16912,#240,.T.);
#21417=EDGE_CURVE('',#16912,#16908,#10106,.T.);
#21418=EDGE_CURVE('',#16911,#16913,#14364,.T.);
#21419=EDGE_CURVE('',#16913,#16914,#241,.F.);
#21420=EDGE_CURVE('',#16914,#16915,#14365,.T.);
#21421=EDGE_CURVE('',#16915,#16912,#242,.T.);
#21422=EDGE_CURVE('',#16913,#16889,#10107,.T.);
#21423=EDGE_CURVE('',#16914,#16895,#10108,.T.);
#21424=EDGE_CURVE('',#16895,#16913,#10109,.T.);
#21425=EDGE_CURVE('',#16916,#16914,#10110,.T.);
#21426=EDGE_CURVE('',#16894,#16916,#661,.T.);
#21427=EDGE_CURVE('',#16800,#16917,#10111,.T.);
#21428=EDGE_CURVE('',#16917,#16779,#662,.T.);
#21429=EDGE_CURVE('',#16791,#16918,#663,.T.);
#21430=EDGE_CURVE('',#16918,#16799,#10112,.T.);
#21431=EDGE_CURVE('',#16866,#16919,#10113,.T.);
#21432=EDGE_CURVE('',#16919,#16920,#664,.T.);
#21433=EDGE_CURVE('',#16920,#16822,#10114,.T.);
#21434=EDGE_CURVE('',#16881,#16921,#10115,.T.);
#21435=EDGE_CURVE('',#16921,#16855,#665,.T.);
#21436=EDGE_CURVE('',#16872,#16922,#666,.T.);
#21437=EDGE_CURVE('',#16922,#16880,#10116,.T.);
#21438=EDGE_CURVE('',#16923,#16924,#10117,.T.);
#21439=EDGE_CURVE('',#16924,#16925,#10118,.T.);
#21440=EDGE_CURVE('',#16925,#16926,#243,.T.);
#21441=EDGE_CURVE('',#16926,#16927,#10119,.T.);
#21442=EDGE_CURVE('',#16927,#16923,#667,.T.);
#21443=EDGE_CURVE('',#16875,#16923,#244,.T.);
#21444=EDGE_CURVE('',#16927,#16922,#14366,.T.);
#21445=EDGE_CURVE('',#16928,#16856,#14367,.T.);
#21446=EDGE_CURVE('',#16921,#16920,#14368,.T.);
#21447=EDGE_CURVE('',#16919,#16928,#245,.T.);
#21448=EDGE_CURVE('',#16823,#16929,#10120,.T.);
#21449=EDGE_CURVE('',#16929,#16930,#668,.T.);
#21450=EDGE_CURVE('',#16930,#16819,#10121,.T.);
#21451=EDGE_CURVE('',#16794,#16930,#246,.T.);
#21452=EDGE_CURVE('',#16929,#16918,#14369,.T.);
#21453=EDGE_CURVE('',#16917,#16916,#14370,.T.);
#21454=EDGE_CURVE('',#16915,#16931,#10122,.T.);
#21455=EDGE_CURVE('',#16931,#16909,#669,.T.);
#21456=EDGE_CURVE('',#16932,#16926,#14371,.T.);
#21457=EDGE_CURVE('',#16933,#16932,#10123,.T.);
#21458=EDGE_CURVE('',#16934,#16933,#14372,.T.);
#21459=EDGE_CURVE('',#16935,#16934,#10124,.T.);
#21460=EDGE_CURVE('',#16936,#16935,#14373,.T.);
#21461=EDGE_CURVE('',#16937,#16936,#10125,.T.);
#21462=EDGE_CURVE('',#16938,#16937,#14374,.T.);
#21463=EDGE_CURVE('',#16938,#16939,#10126,.T.);
#21464=EDGE_CURVE('',#16939,#16940,#14375,.T.);
#21465=EDGE_CURVE('',#16940,#16939,#14376,.T.);
#21466=EDGE_CURVE('',#16931,#16938,#14377,.T.);
#21467=EDGE_CURVE('',#16941,#16925,#670,.T.);
#21468=EDGE_CURVE('',#16941,#16942,#14378,.T.);
#21469=EDGE_CURVE('',#16942,#16932,#247,.F.);
#21470=EDGE_CURVE('',#16924,#16943,#10127,.T.);
#21471=EDGE_CURVE('',#16943,#16944,#248,.T.);
#21472=EDGE_CURVE('',#16944,#16941,#10128,.T.);
#21473=EDGE_CURVE('',#16877,#16945,#10129,.T.);
#21474=EDGE_CURVE('',#16945,#16946,#249,.T.);
#21475=EDGE_CURVE('',#16946,#16878,#10130,.T.);
#21476=EDGE_CURVE('',#16840,#16876,#10131,.T.);
#21477=EDGE_CURVE('',#16947,#16945,#250,.T.);
#21478=EDGE_CURVE('',#16948,#16947,#251,.T.);
#21479=EDGE_CURVE('',#16948,#16949,#252,.T.);
#21480=EDGE_CURVE('',#16950,#16949,#253,.T.);
#21481=EDGE_CURVE('',#16944,#16950,#14379,.T.);
#21482=EDGE_CURVE('',#16943,#16946,#254,.T.);
#21483=EDGE_CURVE('',#16951,#16839,#10132,.T.);
#21484=EDGE_CURVE('',#16952,#16951,#10133,.T.);
#21485=EDGE_CURVE('',#16947,#16952,#10134,.T.);
#21486=EDGE_CURVE('',#16936,#16906,#10135,.T.);
#21487=EDGE_CURVE('',#16953,#16936,#255,.F.);
#21488=EDGE_CURVE('',#16906,#16953,#10136,.T.);
#21489=EDGE_CURVE('',#16935,#16954,#256,.F.);
#21490=EDGE_CURVE('',#16955,#16935,#10137,.T.);
#21491=EDGE_CURVE('',#16954,#16955,#10138,.T.);
#21492=EDGE_CURVE('',#16956,#16955,#10139,.T.);
#21493=EDGE_CURVE('',#16934,#16956,#671,.T.);
#21494=EDGE_CURVE('',#16932,#16957,#10140,.T.);
#21495=EDGE_CURVE('',#16957,#16942,#10141,.T.);
#21496=EDGE_CURVE('',#16949,#16957,#10142,.T.);
#21497=EDGE_CURVE('',#16942,#16950,#10143,.T.);
#21498=EDGE_CURVE('',#16957,#16958,#10144,.T.);
#21499=EDGE_CURVE('',#16958,#16933,#672,.T.);
#21500=EDGE_CURVE('',#16958,#16959,#257,.T.);
#21501=EDGE_CURVE('',#16959,#16960,#14380,.T.);
#21502=EDGE_CURVE('',#16960,#16956,#258,.T.);
#21503=EDGE_CURVE('',#16961,#16962,#259,.T.);
#21504=EDGE_CURVE('',#16962,#16954,#10145,.T.);
#21505=EDGE_CURVE('',#16955,#16961,#10146,.T.);
#21506=EDGE_CURVE('',#16954,#16953,#14381,.T.);
#21507=EDGE_CURVE('',#16963,#16907,#260,.T.);
#21508=EDGE_CURVE('',#16953,#16963,#10147,.T.);
#21509=EDGE_CURVE('',#16905,#16937,#673,.T.);
#21510=EDGE_CURVE('',#16904,#16910,#14382,.T.);
#21511=EDGE_CURVE('',#16898,#16964,#261,.T.);
#21512=EDGE_CURVE('',#16964,#16965,#10148,.T.);
#21513=EDGE_CURVE('',#16965,#16899,#10149,.T.);
#21514=EDGE_CURVE('',#16900,#16951,#10150,.T.);
#21515=EDGE_CURVE('',#16966,#16900,#10151,.T.);
#21516=EDGE_CURVE('',#16951,#16966,#10152,.T.);
#21517=EDGE_CURVE('',#16967,#16966,#10153,.T.);
#21518=EDGE_CURVE('',#16965,#16967,#10154,.T.);
#21519=EDGE_CURVE('',#16968,#16948,#10155,.T.);
#21520=EDGE_CURVE('',#16952,#16968,#10156,.T.);
#21521=EDGE_CURVE('',#16966,#16969,#10157,.T.);
#21522=EDGE_CURVE('',#16969,#16968,#10158,.T.);
#21523=EDGE_CURVE('',#16962,#16963,#14383,.T.);
#21524=EDGE_CURVE('',#16961,#16964,#262,.T.);
#21525=EDGE_CURVE('',#16970,#16970,#14384,.T.);
#21526=EDGE_CURVE('',#16970,#16940,#10159,.T.);
#21527=EDGE_CURVE('',#16969,#16959,#10160,.T.);
#21528=EDGE_CURVE('',#16960,#16967,#10161,.T.);
#21529=EDGE_CURVE('',#16863,#16928,#10162,.T.);
#29802=ORIENTED_EDGE('',*,*,#21215,.T.);
#29803=ORIENTED_EDGE('',*,*,#21216,.T.);
#29804=ORIENTED_EDGE('',*,*,#21217,.T.);
#29805=ORIENTED_EDGE('',*,*,#21218,.T.);
#29806=ORIENTED_EDGE('',*,*,#21219,.T.);
#29807=ORIENTED_EDGE('',*,*,#21216,.F.);
#29808=ORIENTED_EDGE('',*,*,#21220,.T.);
#29809=ORIENTED_EDGE('',*,*,#21221,.F.);
#29810=ORIENTED_EDGE('',*,*,#21222,.F.);
#29811=ORIENTED_EDGE('',*,*,#21215,.F.);
#29812=ORIENTED_EDGE('',*,*,#21223,.T.);
#29813=ORIENTED_EDGE('',*,*,#21224,.F.);
#29814=ORIENTED_EDGE('',*,*,#21225,.F.);
#29815=ORIENTED_EDGE('',*,*,#21226,.F.);
#29816=ORIENTED_EDGE('',*,*,#21227,.T.);
#29817=ORIENTED_EDGE('',*,*,#21228,.F.);
#29818=ORIENTED_EDGE('',*,*,#21220,.F.);
#29819=ORIENTED_EDGE('',*,*,#21219,.F.);
#29820=ORIENTED_EDGE('',*,*,#21229,.F.);
#29821=ORIENTED_EDGE('',*,*,#21230,.F.);
#29822=ORIENTED_EDGE('',*,*,#21231,.T.);
#29823=ORIENTED_EDGE('',*,*,#21232,.F.);
#29824=ORIENTED_EDGE('',*,*,#21233,.F.);
#29825=ORIENTED_EDGE('',*,*,#21223,.F.);
#29826=ORIENTED_EDGE('',*,*,#21224,.T.);
#29827=ORIENTED_EDGE('',*,*,#21233,.T.);
#29828=ORIENTED_EDGE('',*,*,#21234,.T.);
#29829=ORIENTED_EDGE('',*,*,#21235,.T.);
#29830=ORIENTED_EDGE('',*,*,#21236,.T.);
#29831=ORIENTED_EDGE('',*,*,#21226,.T.);
#29832=ORIENTED_EDGE('',*,*,#21237,.T.);
#29833=ORIENTED_EDGE('',*,*,#21238,.T.);
#29834=ORIENTED_EDGE('',*,*,#21239,.T.);
#29835=ORIENTED_EDGE('',*,*,#21240,.T.);
#29836=ORIENTED_EDGE('',*,*,#21241,.T.);
#29837=ORIENTED_EDGE('',*,*,#21242,.T.);
#29838=ORIENTED_EDGE('',*,*,#21243,.T.);
#29839=ORIENTED_EDGE('',*,*,#21238,.F.);
#29840=ORIENTED_EDGE('',*,*,#21236,.F.);
#29841=ORIENTED_EDGE('',*,*,#21243,.F.);
#29842=ORIENTED_EDGE('',*,*,#21244,.T.);
#29843=ORIENTED_EDGE('',*,*,#21245,.F.);
#29844=ORIENTED_EDGE('',*,*,#21246,.F.);
#29845=ORIENTED_EDGE('',*,*,#21247,.F.);
#29846=ORIENTED_EDGE('',*,*,#21227,.F.);
#29847=ORIENTED_EDGE('',*,*,#21242,.F.);
#29848=ORIENTED_EDGE('',*,*,#21248,.F.);
#29849=ORIENTED_EDGE('',*,*,#21249,.F.);
#29850=ORIENTED_EDGE('',*,*,#21250,.F.);
#29851=ORIENTED_EDGE('',*,*,#21244,.F.);
#29852=ORIENTED_EDGE('',*,*,#21241,.F.);
#29853=ORIENTED_EDGE('',*,*,#21251,.T.);
#29854=ORIENTED_EDGE('',*,*,#21252,.T.);
#29855=ORIENTED_EDGE('',*,*,#21253,.F.);
#29856=ORIENTED_EDGE('',*,*,#21254,.T.);
#29857=ORIENTED_EDGE('',*,*,#21248,.T.);
#29858=ORIENTED_EDGE('',*,*,#21255,.T.);
#29859=ORIENTED_EDGE('',*,*,#21221,.T.);
#29860=ORIENTED_EDGE('',*,*,#21228,.T.);
#29861=ORIENTED_EDGE('',*,*,#21247,.T.);
#29862=ORIENTED_EDGE('',*,*,#21256,.T.);
#29863=ORIENTED_EDGE('',*,*,#21217,.F.);
#29864=ORIENTED_EDGE('',*,*,#21222,.T.);
#29865=ORIENTED_EDGE('',*,*,#21255,.F.);
#29866=ORIENTED_EDGE('',*,*,#21257,.T.);
#29867=ORIENTED_EDGE('',*,*,#21258,.T.);
#29868=ORIENTED_EDGE('',*,*,#21259,.F.);
#29869=ORIENTED_EDGE('',*,*,#21260,.T.);
#29870=ORIENTED_EDGE('',*,*,#21261,.T.);
#29871=ORIENTED_EDGE('',*,*,#21262,.T.);
#29872=ORIENTED_EDGE('',*,*,#21263,.T.);
#29873=ORIENTED_EDGE('',*,*,#21264,.T.);
#29874=ORIENTED_EDGE('',*,*,#21261,.F.);
#29875=ORIENTED_EDGE('',*,*,#21265,.F.);
#29876=ORIENTED_EDGE('',*,*,#21266,.F.);
#29877=ORIENTED_EDGE('',*,*,#21267,.T.);
#29878=ORIENTED_EDGE('',*,*,#21268,.F.);
#29879=ORIENTED_EDGE('',*,*,#21269,.F.);
#29880=ORIENTED_EDGE('',*,*,#21270,.F.);
#29881=ORIENTED_EDGE('',*,*,#21271,.T.);
#29882=ORIENTED_EDGE('',*,*,#21260,.F.);
#29883=ORIENTED_EDGE('',*,*,#21272,.F.);
#29884=ORIENTED_EDGE('',*,*,#21273,.T.);
#29885=ORIENTED_EDGE('',*,*,#21274,.T.);
#29886=ORIENTED_EDGE('',*,*,#21275,.F.);
#29887=ORIENTED_EDGE('',*,*,#21265,.T.);
#29888=ORIENTED_EDGE('',*,*,#21264,.F.);
#29889=ORIENTED_EDGE('',*,*,#21276,.T.);
#29890=ORIENTED_EDGE('',*,*,#21234,.F.);
#29891=ORIENTED_EDGE('',*,*,#21232,.T.);
#29892=ORIENTED_EDGE('',*,*,#21277,.T.);
#29893=ORIENTED_EDGE('',*,*,#21272,.T.);
#29894=ORIENTED_EDGE('',*,*,#21278,.T.);
#29895=ORIENTED_EDGE('',*,*,#21279,.T.);
#29896=ORIENTED_EDGE('',*,*,#21280,.T.);
#29897=ORIENTED_EDGE('',*,*,#21281,.T.);
#29898=ORIENTED_EDGE('',*,*,#21282,.T.);
#29899=ORIENTED_EDGE('',*,*,#21280,.F.);
#29900=ORIENTED_EDGE('',*,*,#21283,.T.);
#29901=ORIENTED_EDGE('',*,*,#21284,.F.);
#29902=ORIENTED_EDGE('',*,*,#21285,.T.);
#29903=ORIENTED_EDGE('',*,*,#21286,.T.);
#29904=ORIENTED_EDGE('',*,*,#21287,.T.);
#29905=ORIENTED_EDGE('',*,*,#21279,.F.);
#29906=ORIENTED_EDGE('',*,*,#21288,.T.);
#29907=ORIENTED_EDGE('',*,*,#21289,.F.);
#29908=ORIENTED_EDGE('',*,*,#21283,.F.);
#29909=ORIENTED_EDGE('',*,*,#21278,.F.);
#29910=ORIENTED_EDGE('',*,*,#21290,.T.);
#29911=ORIENTED_EDGE('',*,*,#21291,.F.);
#29912=ORIENTED_EDGE('',*,*,#21292,.F.);
#29913=ORIENTED_EDGE('',*,*,#21293,.F.);
#29914=ORIENTED_EDGE('',*,*,#21294,.T.);
#29915=ORIENTED_EDGE('',*,*,#21295,.F.);
#29916=ORIENTED_EDGE('',*,*,#21288,.F.);
#29917=ORIENTED_EDGE('',*,*,#21296,.T.);
#29918=ORIENTED_EDGE('',*,*,#21291,.T.);
#29919=ORIENTED_EDGE('',*,*,#21297,.T.);
#29920=ORIENTED_EDGE('',*,*,#21253,.T.);
#29921=ORIENTED_EDGE('',*,*,#21240,.F.);
#29922=ORIENTED_EDGE('',*,*,#21298,.T.);
#29923=ORIENTED_EDGE('',*,*,#21299,.T.);
#29924=ORIENTED_EDGE('',*,*,#21300,.T.);
#29925=ORIENTED_EDGE('',*,*,#21251,.F.);
#29926=ORIENTED_EDGE('',*,*,#21296,.F.);
#29927=ORIENTED_EDGE('',*,*,#21252,.F.);
#29928=ORIENTED_EDGE('',*,*,#21300,.F.);
#29929=ORIENTED_EDGE('',*,*,#21301,.T.);
#29930=ORIENTED_EDGE('',*,*,#21302,.F.);
#29931=ORIENTED_EDGE('',*,*,#21303,.F.);
#29932=ORIENTED_EDGE('',*,*,#21304,.F.);
#29933=ORIENTED_EDGE('',*,*,#21292,.T.);
#29934=ORIENTED_EDGE('',*,*,#21305,.F.);
#29935=ORIENTED_EDGE('',*,*,#21306,.T.);
#29936=ORIENTED_EDGE('',*,*,#21307,.F.);
#29937=ORIENTED_EDGE('',*,*,#21262,.F.);
#29938=ORIENTED_EDGE('',*,*,#21271,.F.);
#29939=ORIENTED_EDGE('',*,*,#21308,.F.);
#29940=ORIENTED_EDGE('',*,*,#21309,.F.);
#29941=ORIENTED_EDGE('',*,*,#21310,.F.);
#29942=ORIENTED_EDGE('',*,*,#21311,.F.);
#29943=ORIENTED_EDGE('',*,*,#21312,.F.);
#29944=ORIENTED_EDGE('',*,*,#21313,.F.);
#29945=ORIENTED_EDGE('',*,*,#21314,.F.);
#29946=ORIENTED_EDGE('',*,*,#21301,.F.);
#29947=ORIENTED_EDGE('',*,*,#21299,.F.);
#29948=ORIENTED_EDGE('',*,*,#21315,.F.);
#29949=ORIENTED_EDGE('',*,*,#21306,.F.);
#29950=ORIENTED_EDGE('',*,*,#21316,.T.);
#29951=ORIENTED_EDGE('',*,*,#21317,.T.);
#29952=ORIENTED_EDGE('',*,*,#21318,.T.);
#29953=ORIENTED_EDGE('',*,*,#21319,.T.);
#29954=ORIENTED_EDGE('',*,*,#21320,.T.);
#29955=ORIENTED_EDGE('',*,*,#21317,.F.);
#29956=ORIENTED_EDGE('',*,*,#21321,.T.);
#29957=ORIENTED_EDGE('',*,*,#21322,.F.);
#29958=ORIENTED_EDGE('',*,*,#21323,.F.);
#29959=ORIENTED_EDGE('',*,*,#21316,.F.);
#29960=ORIENTED_EDGE('',*,*,#21324,.T.);
#29961=ORIENTED_EDGE('',*,*,#21325,.F.);
#29962=ORIENTED_EDGE('',*,*,#21326,.F.);
#29963=ORIENTED_EDGE('',*,*,#21327,.F.);
#29964=ORIENTED_EDGE('',*,*,#21328,.T.);
#29965=ORIENTED_EDGE('',*,*,#21329,.F.);
#29966=ORIENTED_EDGE('',*,*,#21321,.F.);
#29967=ORIENTED_EDGE('',*,*,#21320,.F.);
#29968=ORIENTED_EDGE('',*,*,#21330,.F.);
#29969=ORIENTED_EDGE('',*,*,#21331,.F.);
#29970=ORIENTED_EDGE('',*,*,#21332,.T.);
#29971=ORIENTED_EDGE('',*,*,#21333,.F.);
#29972=ORIENTED_EDGE('',*,*,#21334,.F.);
#29973=ORIENTED_EDGE('',*,*,#21324,.F.);
#29974=ORIENTED_EDGE('',*,*,#21335,.T.);
#29975=ORIENTED_EDGE('',*,*,#21325,.T.);
#29976=ORIENTED_EDGE('',*,*,#21334,.T.);
#29977=ORIENTED_EDGE('',*,*,#21336,.T.);
#29978=ORIENTED_EDGE('',*,*,#21337,.F.);
#29979=ORIENTED_EDGE('',*,*,#21338,.F.);
#29980=ORIENTED_EDGE('',*,*,#21339,.F.);
#29981=ORIENTED_EDGE('',*,*,#21340,.T.);
#29982=ORIENTED_EDGE('',*,*,#21338,.T.);
#29983=ORIENTED_EDGE('',*,*,#21341,.T.);
#29984=ORIENTED_EDGE('',*,*,#21336,.F.);
#29985=ORIENTED_EDGE('',*,*,#21333,.T.);
#29986=ORIENTED_EDGE('',*,*,#21342,.T.);
#29987=ORIENTED_EDGE('',*,*,#21293,.T.);
#29988=ORIENTED_EDGE('',*,*,#21304,.T.);
#29989=ORIENTED_EDGE('',*,*,#21343,.T.);
#29990=ORIENTED_EDGE('',*,*,#21303,.T.);
#29991=ORIENTED_EDGE('',*,*,#21339,.T.);
#29992=ORIENTED_EDGE('',*,*,#21344,.T.);
#29993=ORIENTED_EDGE('',*,*,#21345,.T.);
#29994=ORIENTED_EDGE('',*,*,#21343,.F.);
#29995=ORIENTED_EDGE('',*,*,#21314,.T.);
#29996=ORIENTED_EDGE('',*,*,#21346,.T.);
#29997=ORIENTED_EDGE('',*,*,#21337,.T.);
#29998=ORIENTED_EDGE('',*,*,#21302,.T.);
#29999=ORIENTED_EDGE('',*,*,#21335,.F.);
#30000=ORIENTED_EDGE('',*,*,#21341,.F.);
#30001=ORIENTED_EDGE('',*,*,#21346,.F.);
#30002=ORIENTED_EDGE('',*,*,#21313,.T.);
#30003=ORIENTED_EDGE('',*,*,#21347,.F.);
#30004=ORIENTED_EDGE('',*,*,#21348,.F.);
#30005=ORIENTED_EDGE('',*,*,#21349,.F.);
#30006=ORIENTED_EDGE('',*,*,#21326,.T.);
#30007=ORIENTED_EDGE('',*,*,#21284,.T.);
#30008=ORIENTED_EDGE('',*,*,#21289,.T.);
#30009=ORIENTED_EDGE('',*,*,#21295,.T.);
#30010=ORIENTED_EDGE('',*,*,#21350,.T.);
#30011=ORIENTED_EDGE('',*,*,#21351,.T.);
#30012=ORIENTED_EDGE('',*,*,#21352,.T.);
#30013=ORIENTED_EDGE('',*,*,#21327,.T.);
#30014=ORIENTED_EDGE('',*,*,#21349,.T.);
#30015=ORIENTED_EDGE('',*,*,#21353,.T.);
#30016=ORIENTED_EDGE('',*,*,#21348,.T.);
#30017=ORIENTED_EDGE('',*,*,#21354,.T.);
#30018=ORIENTED_EDGE('',*,*,#21355,.T.);
#30019=ORIENTED_EDGE('',*,*,#21356,.T.);
#30020=ORIENTED_EDGE('',*,*,#21357,.T.);
#30021=ORIENTED_EDGE('',*,*,#21353,.F.);
#30022=ORIENTED_EDGE('',*,*,#21352,.F.);
#30023=ORIENTED_EDGE('',*,*,#21357,.F.);
#30024=ORIENTED_EDGE('',*,*,#21358,.T.);
#30025=ORIENTED_EDGE('',*,*,#21359,.F.);
#30026=ORIENTED_EDGE('',*,*,#21360,.F.);
#30027=ORIENTED_EDGE('',*,*,#21361,.F.);
#30028=ORIENTED_EDGE('',*,*,#21328,.F.);
#30029=ORIENTED_EDGE('',*,*,#21356,.F.);
#30030=ORIENTED_EDGE('',*,*,#21362,.F.);
#30031=ORIENTED_EDGE('',*,*,#21363,.F.);
#30032=ORIENTED_EDGE('',*,*,#21364,.F.);
#30033=ORIENTED_EDGE('',*,*,#21358,.F.);
#30034=ORIENTED_EDGE('',*,*,#21355,.F.);
#30035=ORIENTED_EDGE('',*,*,#21365,.T.);
#30036=ORIENTED_EDGE('',*,*,#21366,.T.);
#30037=ORIENTED_EDGE('',*,*,#21367,.F.);
#30038=ORIENTED_EDGE('',*,*,#21368,.T.);
#30039=ORIENTED_EDGE('',*,*,#21362,.T.);
#30040=ORIENTED_EDGE('',*,*,#21369,.T.);
#30041=ORIENTED_EDGE('',*,*,#21322,.T.);
#30042=ORIENTED_EDGE('',*,*,#21329,.T.);
#30043=ORIENTED_EDGE('',*,*,#21361,.T.);
#30044=ORIENTED_EDGE('',*,*,#21370,.T.);
#30045=ORIENTED_EDGE('',*,*,#21318,.F.);
#30046=ORIENTED_EDGE('',*,*,#21323,.T.);
#30047=ORIENTED_EDGE('',*,*,#21369,.F.);
#30048=ORIENTED_EDGE('',*,*,#21371,.T.);
#30049=ORIENTED_EDGE('',*,*,#21372,.T.);
#30050=ORIENTED_EDGE('',*,*,#21373,.F.);
#30051=ORIENTED_EDGE('',*,*,#21374,.T.);
#30052=ORIENTED_EDGE('',*,*,#21269,.T.);
#30053=ORIENTED_EDGE('',*,*,#21375,.T.);
#30054=ORIENTED_EDGE('',*,*,#21376,.T.);
#30055=ORIENTED_EDGE('',*,*,#21377,.T.);
#30056=ORIENTED_EDGE('',*,*,#21378,.T.);
#30057=ORIENTED_EDGE('',*,*,#21374,.F.);
#30058=ORIENTED_EDGE('',*,*,#21379,.T.);
#30059=ORIENTED_EDGE('',*,*,#21380,.T.);
#30060=ORIENTED_EDGE('',*,*,#21308,.T.);
#30061=ORIENTED_EDGE('',*,*,#21270,.T.);
#30062=ORIENTED_EDGE('',*,*,#21381,.T.);
#30063=ORIENTED_EDGE('',*,*,#21382,.T.);
#30064=ORIENTED_EDGE('',*,*,#21266,.T.);
#30065=ORIENTED_EDGE('',*,*,#21275,.T.);
#30066=ORIENTED_EDGE('',*,*,#21382,.F.);
#30067=ORIENTED_EDGE('',*,*,#21383,.T.);
#30068=ORIENTED_EDGE('',*,*,#21384,.F.);
#30069=ORIENTED_EDGE('',*,*,#21385,.F.);
#30070=ORIENTED_EDGE('',*,*,#21386,.F.);
#30071=ORIENTED_EDGE('',*,*,#21387,.T.);
#30072=ORIENTED_EDGE('',*,*,#21388,.F.);
#30073=ORIENTED_EDGE('',*,*,#21267,.F.);
#30074=ORIENTED_EDGE('',*,*,#21381,.F.);
#30075=ORIENTED_EDGE('',*,*,#21274,.F.);
#30076=ORIENTED_EDGE('',*,*,#21389,.T.);
#30077=ORIENTED_EDGE('',*,*,#21390,.F.);
#30078=ORIENTED_EDGE('',*,*,#21391,.F.);
#30079=ORIENTED_EDGE('',*,*,#21392,.F.);
#30080=ORIENTED_EDGE('',*,*,#21383,.F.);
#30081=ORIENTED_EDGE('',*,*,#21273,.F.);
#30082=ORIENTED_EDGE('',*,*,#21277,.F.);
#30083=ORIENTED_EDGE('',*,*,#21231,.F.);
#30084=ORIENTED_EDGE('',*,*,#21393,.F.);
#30085=ORIENTED_EDGE('',*,*,#21389,.F.);
#30086=ORIENTED_EDGE('',*,*,#21380,.F.);
#30087=ORIENTED_EDGE('',*,*,#21394,.F.);
#30088=ORIENTED_EDGE('',*,*,#21395,.F.);
#30089=ORIENTED_EDGE('',*,*,#21396,.T.);
#30090=ORIENTED_EDGE('',*,*,#21397,.F.);
#30091=ORIENTED_EDGE('',*,*,#21398,.F.);
#30092=ORIENTED_EDGE('',*,*,#21399,.F.);
#30093=ORIENTED_EDGE('',*,*,#21309,.T.);
#30094=ORIENTED_EDGE('',*,*,#21378,.F.);
#30095=ORIENTED_EDGE('',*,*,#21400,.T.);
#30096=ORIENTED_EDGE('',*,*,#21401,.T.);
#30097=ORIENTED_EDGE('',*,*,#21402,.F.);
#30098=ORIENTED_EDGE('',*,*,#21394,.T.);
#30099=ORIENTED_EDGE('',*,*,#21379,.F.);
#30100=ORIENTED_EDGE('',*,*,#21403,.T.);
#30101=ORIENTED_EDGE('',*,*,#21395,.T.);
#30102=ORIENTED_EDGE('',*,*,#21402,.T.);
#30103=ORIENTED_EDGE('',*,*,#21404,.T.);
#30104=ORIENTED_EDGE('',*,*,#21404,.F.);
#30105=ORIENTED_EDGE('',*,*,#21401,.F.);
#30106=ORIENTED_EDGE('',*,*,#21405,.T.);
#30107=ORIENTED_EDGE('',*,*,#21406,.F.);
#30108=ORIENTED_EDGE('',*,*,#21407,.F.);
#30109=ORIENTED_EDGE('',*,*,#21408,.F.);
#30110=ORIENTED_EDGE('',*,*,#21409,.F.);
#30111=ORIENTED_EDGE('',*,*,#21388,.T.);
#30112=ORIENTED_EDGE('',*,*,#21410,.T.);
#30113=ORIENTED_EDGE('',*,*,#21375,.F.);
#30114=ORIENTED_EDGE('',*,*,#21268,.T.);
#30115=ORIENTED_EDGE('',*,*,#21410,.F.);
#30116=ORIENTED_EDGE('',*,*,#21387,.F.);
#30117=ORIENTED_EDGE('',*,*,#21411,.F.);
#30118=ORIENTED_EDGE('',*,*,#21412,.F.);
#30119=ORIENTED_EDGE('',*,*,#21413,.F.);
#30120=ORIENTED_EDGE('',*,*,#21414,.T.);
#30121=ORIENTED_EDGE('',*,*,#21376,.F.);
#30122=ORIENTED_EDGE('',*,*,#21386,.T.);
#30123=ORIENTED_EDGE('',*,*,#21415,.T.);
#30124=ORIENTED_EDGE('',*,*,#21416,.T.);
#30125=ORIENTED_EDGE('',*,*,#21417,.T.);
#30126=ORIENTED_EDGE('',*,*,#21411,.T.);
#30127=ORIENTED_EDGE('',*,*,#21416,.F.);
#30128=ORIENTED_EDGE('',*,*,#21418,.T.);
#30129=ORIENTED_EDGE('',*,*,#21419,.T.);
#30130=ORIENTED_EDGE('',*,*,#21420,.T.);
#30131=ORIENTED_EDGE('',*,*,#21421,.T.);
#30132=ORIENTED_EDGE('',*,*,#21415,.F.);
#30133=ORIENTED_EDGE('',*,*,#21385,.T.);
#30134=ORIENTED_EDGE('',*,*,#21422,.F.);
#30135=ORIENTED_EDGE('',*,*,#21418,.F.);
#30136=ORIENTED_EDGE('',*,*,#21423,.F.);
#30137=ORIENTED_EDGE('',*,*,#21419,.F.);
#30138=ORIENTED_EDGE('',*,*,#21424,.F.);
#30139=ORIENTED_EDGE('',*,*,#21384,.T.);
#30140=ORIENTED_EDGE('',*,*,#21392,.T.);
#30141=ORIENTED_EDGE('',*,*,#21424,.T.);
#30142=ORIENTED_EDGE('',*,*,#21422,.T.);
#30143=ORIENTED_EDGE('',*,*,#21425,.T.);
#30144=ORIENTED_EDGE('',*,*,#21423,.T.);
#30145=ORIENTED_EDGE('',*,*,#21391,.T.);
#30146=ORIENTED_EDGE('',*,*,#21426,.T.);
#30147=ORIENTED_EDGE('',*,*,#21218,.F.);
#30148=ORIENTED_EDGE('',*,*,#21259,.T.);
#30149=ORIENTED_EDGE('',*,*,#21427,.T.);
#30150=ORIENTED_EDGE('',*,*,#21428,.T.);
#30151=ORIENTED_EDGE('',*,*,#21229,.T.);
#30152=ORIENTED_EDGE('',*,*,#21256,.F.);
#30153=ORIENTED_EDGE('',*,*,#21246,.T.);
#30154=ORIENTED_EDGE('',*,*,#21429,.T.);
#30155=ORIENTED_EDGE('',*,*,#21430,.T.);
#30156=ORIENTED_EDGE('',*,*,#21257,.F.);
#30157=ORIENTED_EDGE('',*,*,#21351,.F.);
#30158=ORIENTED_EDGE('',*,*,#21431,.T.);
#30159=ORIENTED_EDGE('',*,*,#21432,.T.);
#30160=ORIENTED_EDGE('',*,*,#21433,.T.);
#30161=ORIENTED_EDGE('',*,*,#21285,.F.);
#30162=ORIENTED_EDGE('',*,*,#21319,.F.);
#30163=ORIENTED_EDGE('',*,*,#21373,.T.);
#30164=ORIENTED_EDGE('',*,*,#21434,.T.);
#30165=ORIENTED_EDGE('',*,*,#21435,.T.);
#30166=ORIENTED_EDGE('',*,*,#21330,.T.);
#30167=ORIENTED_EDGE('',*,*,#21370,.F.);
#30168=ORIENTED_EDGE('',*,*,#21360,.T.);
#30169=ORIENTED_EDGE('',*,*,#21436,.T.);
#30170=ORIENTED_EDGE('',*,*,#21437,.T.);
#30171=ORIENTED_EDGE('',*,*,#21371,.F.);
#30172=ORIENTED_EDGE('',*,*,#21438,.T.);
#30173=ORIENTED_EDGE('',*,*,#21439,.T.);
#30174=ORIENTED_EDGE('',*,*,#21440,.T.);
#30175=ORIENTED_EDGE('',*,*,#21441,.T.);
#30176=ORIENTED_EDGE('',*,*,#21442,.T.);
#30177=ORIENTED_EDGE('',*,*,#21364,.T.);
#30178=ORIENTED_EDGE('',*,*,#21443,.T.);
#30179=ORIENTED_EDGE('',*,*,#21442,.F.);
#30180=ORIENTED_EDGE('',*,*,#21444,.T.);
#30181=ORIENTED_EDGE('',*,*,#21436,.F.);
#30182=ORIENTED_EDGE('',*,*,#21359,.T.);
#30183=ORIENTED_EDGE('',*,*,#21445,.T.);
#30184=ORIENTED_EDGE('',*,*,#21331,.T.);
#30185=ORIENTED_EDGE('',*,*,#21435,.F.);
#30186=ORIENTED_EDGE('',*,*,#21446,.T.);
#30187=ORIENTED_EDGE('',*,*,#21432,.F.);
#30188=ORIENTED_EDGE('',*,*,#21447,.T.);
#30189=ORIENTED_EDGE('',*,*,#21281,.F.);
#30190=ORIENTED_EDGE('',*,*,#21287,.F.);
#30191=ORIENTED_EDGE('',*,*,#21448,.T.);
#30192=ORIENTED_EDGE('',*,*,#21449,.T.);
#30193=ORIENTED_EDGE('',*,*,#21450,.T.);
#30194=ORIENTED_EDGE('',*,*,#21250,.T.);
#30195=ORIENTED_EDGE('',*,*,#21451,.T.);
#30196=ORIENTED_EDGE('',*,*,#21449,.F.);
#30197=ORIENTED_EDGE('',*,*,#21452,.T.);
#30198=ORIENTED_EDGE('',*,*,#21429,.F.);
#30199=ORIENTED_EDGE('',*,*,#21245,.T.);
#30200=ORIENTED_EDGE('',*,*,#21393,.T.);
#30201=ORIENTED_EDGE('',*,*,#21230,.T.);
#30202=ORIENTED_EDGE('',*,*,#21428,.F.);
#30203=ORIENTED_EDGE('',*,*,#21453,.T.);
#30204=ORIENTED_EDGE('',*,*,#21426,.F.);
#30205=ORIENTED_EDGE('',*,*,#21390,.T.);
#30206=ORIENTED_EDGE('',*,*,#21417,.F.);
#30207=ORIENTED_EDGE('',*,*,#21421,.F.);
#30208=ORIENTED_EDGE('',*,*,#21454,.T.);
#30209=ORIENTED_EDGE('',*,*,#21455,.T.);
#30210=ORIENTED_EDGE('',*,*,#21412,.T.);
#30211=ORIENTED_EDGE('',*,*,#21420,.F.);
#30212=ORIENTED_EDGE('',*,*,#21425,.F.);
#30213=ORIENTED_EDGE('',*,*,#21453,.F.);
#30214=ORIENTED_EDGE('',*,*,#21427,.F.);
#30215=ORIENTED_EDGE('',*,*,#21258,.F.);
#30216=ORIENTED_EDGE('',*,*,#21430,.F.);
#30217=ORIENTED_EDGE('',*,*,#21452,.F.);
#30218=ORIENTED_EDGE('',*,*,#21448,.F.);
#30219=ORIENTED_EDGE('',*,*,#21286,.F.);
#30220=ORIENTED_EDGE('',*,*,#21433,.F.);
#30221=ORIENTED_EDGE('',*,*,#21446,.F.);
#30222=ORIENTED_EDGE('',*,*,#21434,.F.);
#30223=ORIENTED_EDGE('',*,*,#21372,.F.);
#30224=ORIENTED_EDGE('',*,*,#21437,.F.);
#30225=ORIENTED_EDGE('',*,*,#21444,.F.);
#30226=ORIENTED_EDGE('',*,*,#21441,.F.);
#30227=ORIENTED_EDGE('',*,*,#21456,.F.);
#30228=ORIENTED_EDGE('',*,*,#21457,.F.);
#30229=ORIENTED_EDGE('',*,*,#21458,.F.);
#30230=ORIENTED_EDGE('',*,*,#21459,.F.);
#30231=ORIENTED_EDGE('',*,*,#21460,.F.);
#30232=ORIENTED_EDGE('',*,*,#21461,.F.);
#30233=ORIENTED_EDGE('',*,*,#21462,.F.);
#30234=ORIENTED_EDGE('',*,*,#21463,.T.);
#30235=ORIENTED_EDGE('',*,*,#21464,.T.);
#30236=ORIENTED_EDGE('',*,*,#21465,.T.);
#30237=ORIENTED_EDGE('',*,*,#21463,.F.);
#30238=ORIENTED_EDGE('',*,*,#21466,.F.);
#30239=ORIENTED_EDGE('',*,*,#21454,.F.);
#30240=ORIENTED_EDGE('',*,*,#21440,.F.);
#30241=ORIENTED_EDGE('',*,*,#21467,.F.);
#30242=ORIENTED_EDGE('',*,*,#21468,.T.);
#30243=ORIENTED_EDGE('',*,*,#21469,.T.);
#30244=ORIENTED_EDGE('',*,*,#21456,.T.);
#30245=ORIENTED_EDGE('',*,*,#21439,.F.);
#30246=ORIENTED_EDGE('',*,*,#21470,.T.);
#30247=ORIENTED_EDGE('',*,*,#21471,.T.);
#30248=ORIENTED_EDGE('',*,*,#21472,.T.);
#30249=ORIENTED_EDGE('',*,*,#21467,.T.);
#30250=ORIENTED_EDGE('',*,*,#21473,.T.);
#30251=ORIENTED_EDGE('',*,*,#21474,.T.);
#30252=ORIENTED_EDGE('',*,*,#21475,.T.);
#30253=ORIENTED_EDGE('',*,*,#21367,.T.);
#30254=ORIENTED_EDGE('',*,*,#21354,.F.);
#30255=ORIENTED_EDGE('',*,*,#21347,.T.);
#30256=ORIENTED_EDGE('',*,*,#21312,.T.);
#30257=ORIENTED_EDGE('',*,*,#21476,.T.);
#30258=ORIENTED_EDGE('',*,*,#21365,.F.);
#30259=ORIENTED_EDGE('',*,*,#21474,.F.);
#30260=ORIENTED_EDGE('',*,*,#21477,.F.);
#30261=ORIENTED_EDGE('',*,*,#21478,.F.);
#30262=ORIENTED_EDGE('',*,*,#21479,.T.);
#30263=ORIENTED_EDGE('',*,*,#21480,.F.);
#30264=ORIENTED_EDGE('',*,*,#21481,.F.);
#30265=ORIENTED_EDGE('',*,*,#21471,.F.);
#30266=ORIENTED_EDGE('',*,*,#21482,.T.);
#30267=ORIENTED_EDGE('',*,*,#21473,.F.);
#30268=ORIENTED_EDGE('',*,*,#21366,.F.);
#30269=ORIENTED_EDGE('',*,*,#21476,.F.);
#30270=ORIENTED_EDGE('',*,*,#21311,.T.);
#30271=ORIENTED_EDGE('',*,*,#21483,.F.);
#30272=ORIENTED_EDGE('',*,*,#21484,.F.);
#30273=ORIENTED_EDGE('',*,*,#21485,.F.);
#30274=ORIENTED_EDGE('',*,*,#21477,.T.);
#30275=ORIENTED_EDGE('',*,*,#21486,.F.);
#30276=ORIENTED_EDGE('',*,*,#21487,.F.);
#30277=ORIENTED_EDGE('',*,*,#21488,.F.);
#30278=ORIENTED_EDGE('',*,*,#21489,.F.);
#30279=ORIENTED_EDGE('',*,*,#21490,.F.);
#30280=ORIENTED_EDGE('',*,*,#21491,.F.);
#30281=ORIENTED_EDGE('',*,*,#21492,.T.);
#30282=ORIENTED_EDGE('',*,*,#21490,.T.);
#30283=ORIENTED_EDGE('',*,*,#21459,.T.);
#30284=ORIENTED_EDGE('',*,*,#21493,.T.);
#30285=ORIENTED_EDGE('',*,*,#21494,.F.);
#30286=ORIENTED_EDGE('',*,*,#21469,.F.);
#30287=ORIENTED_EDGE('',*,*,#21495,.F.);
#30288=ORIENTED_EDGE('',*,*,#21480,.T.);
#30289=ORIENTED_EDGE('',*,*,#21496,.T.);
#30290=ORIENTED_EDGE('',*,*,#21495,.T.);
#30291=ORIENTED_EDGE('',*,*,#21497,.T.);
#30292=ORIENTED_EDGE('',*,*,#21457,.T.);
#30293=ORIENTED_EDGE('',*,*,#21494,.T.);
#30294=ORIENTED_EDGE('',*,*,#21498,.T.);
#30295=ORIENTED_EDGE('',*,*,#21499,.T.);
#30296=ORIENTED_EDGE('',*,*,#21458,.T.);
#30297=ORIENTED_EDGE('',*,*,#21499,.F.);
#30298=ORIENTED_EDGE('',*,*,#21500,.T.);
#30299=ORIENTED_EDGE('',*,*,#21501,.T.);
#30300=ORIENTED_EDGE('',*,*,#21502,.T.);
#30301=ORIENTED_EDGE('',*,*,#21493,.F.);
#30302=ORIENTED_EDGE('',*,*,#21503,.T.);
#30303=ORIENTED_EDGE('',*,*,#21504,.T.);
#30304=ORIENTED_EDGE('',*,*,#21491,.T.);
#30305=ORIENTED_EDGE('',*,*,#21505,.T.);
#30306=ORIENTED_EDGE('',*,*,#21489,.T.);
#30307=ORIENTED_EDGE('',*,*,#21506,.T.);
#30308=ORIENTED_EDGE('',*,*,#21487,.T.);
#30309=ORIENTED_EDGE('',*,*,#21460,.T.);
#30310=ORIENTED_EDGE('',*,*,#21507,.T.);
#30311=ORIENTED_EDGE('',*,*,#21408,.T.);
#30312=ORIENTED_EDGE('',*,*,#21488,.T.);
#30313=ORIENTED_EDGE('',*,*,#21508,.T.);
#30314=ORIENTED_EDGE('',*,*,#21461,.T.);
#30315=ORIENTED_EDGE('',*,*,#21486,.T.);
#30316=ORIENTED_EDGE('',*,*,#21407,.T.);
#30317=ORIENTED_EDGE('',*,*,#21509,.T.);
#30318=ORIENTED_EDGE('',*,*,#21466,.T.);
#30319=ORIENTED_EDGE('',*,*,#21462,.T.);
#30320=ORIENTED_EDGE('',*,*,#21509,.F.);
#30321=ORIENTED_EDGE('',*,*,#21406,.T.);
#30322=ORIENTED_EDGE('',*,*,#21510,.T.);
#30323=ORIENTED_EDGE('',*,*,#21413,.T.);
#30324=ORIENTED_EDGE('',*,*,#21455,.F.);
#30325=ORIENTED_EDGE('',*,*,#21438,.F.);
#30326=ORIENTED_EDGE('',*,*,#21443,.F.);
#30327=ORIENTED_EDGE('',*,*,#21363,.T.);
#30328=ORIENTED_EDGE('',*,*,#21368,.F.);
#30329=ORIENTED_EDGE('',*,*,#21475,.F.);
#30330=ORIENTED_EDGE('',*,*,#21482,.F.);
#30331=ORIENTED_EDGE('',*,*,#21470,.F.);
#30332=ORIENTED_EDGE('',*,*,#21377,.F.);
#30333=ORIENTED_EDGE('',*,*,#21414,.F.);
#30334=ORIENTED_EDGE('',*,*,#21510,.F.);
#30335=ORIENTED_EDGE('',*,*,#21405,.F.);
#30336=ORIENTED_EDGE('',*,*,#21400,.F.);
#30337=ORIENTED_EDGE('',*,*,#21397,.T.);
#30338=ORIENTED_EDGE('',*,*,#21511,.T.);
#30339=ORIENTED_EDGE('',*,*,#21512,.T.);
#30340=ORIENTED_EDGE('',*,*,#21513,.T.);
#30341=ORIENTED_EDGE('',*,*,#21514,.F.);
#30342=ORIENTED_EDGE('',*,*,#21515,.F.);
#30343=ORIENTED_EDGE('',*,*,#21516,.F.);
#30344=ORIENTED_EDGE('',*,*,#21517,.T.);
#30345=ORIENTED_EDGE('',*,*,#21515,.T.);
#30346=ORIENTED_EDGE('',*,*,#21398,.T.);
#30347=ORIENTED_EDGE('',*,*,#21513,.F.);
#30348=ORIENTED_EDGE('',*,*,#21518,.T.);
#30349=ORIENTED_EDGE('',*,*,#21519,.T.);
#30350=ORIENTED_EDGE('',*,*,#21478,.T.);
#30351=ORIENTED_EDGE('',*,*,#21485,.T.);
#30352=ORIENTED_EDGE('',*,*,#21520,.T.);
#30353=ORIENTED_EDGE('',*,*,#21484,.T.);
#30354=ORIENTED_EDGE('',*,*,#21516,.T.);
#30355=ORIENTED_EDGE('',*,*,#21521,.T.);
#30356=ORIENTED_EDGE('',*,*,#21522,.T.);
#30357=ORIENTED_EDGE('',*,*,#21520,.F.);
#30358=ORIENTED_EDGE('',*,*,#21310,.T.);
#30359=ORIENTED_EDGE('',*,*,#21399,.T.);
#30360=ORIENTED_EDGE('',*,*,#21514,.T.);
#30361=ORIENTED_EDGE('',*,*,#21483,.T.);
#30362=ORIENTED_EDGE('',*,*,#21403,.F.);
#30363=ORIENTED_EDGE('',*,*,#21409,.T.);
#30364=ORIENTED_EDGE('',*,*,#21507,.F.);
#30365=ORIENTED_EDGE('',*,*,#21523,.F.);
#30366=ORIENTED_EDGE('',*,*,#21503,.F.);
#30367=ORIENTED_EDGE('',*,*,#21524,.T.);
#30368=ORIENTED_EDGE('',*,*,#21511,.F.);
#30369=ORIENTED_EDGE('',*,*,#21396,.F.);
#30370=ORIENTED_EDGE('',*,*,#21525,.F.);
#30371=ORIENTED_EDGE('',*,*,#21526,.T.);
#30372=ORIENTED_EDGE('',*,*,#21464,.F.);
#30373=ORIENTED_EDGE('',*,*,#21465,.F.);
#30374=ORIENTED_EDGE('',*,*,#21526,.F.);
#30375=ORIENTED_EDGE('',*,*,#21496,.F.);
#30376=ORIENTED_EDGE('',*,*,#21479,.F.);
#30377=ORIENTED_EDGE('',*,*,#21519,.F.);
#30378=ORIENTED_EDGE('',*,*,#21522,.F.);
#30379=ORIENTED_EDGE('',*,*,#21527,.T.);
#30380=ORIENTED_EDGE('',*,*,#21500,.F.);
#30381=ORIENTED_EDGE('',*,*,#21498,.F.);
#30382=ORIENTED_EDGE('',*,*,#21492,.F.);
#30383=ORIENTED_EDGE('',*,*,#21502,.F.);
#30384=ORIENTED_EDGE('',*,*,#21528,.T.);
#30385=ORIENTED_EDGE('',*,*,#21518,.F.);
#30386=ORIENTED_EDGE('',*,*,#21512,.F.);
#30387=ORIENTED_EDGE('',*,*,#21524,.F.);
#30388=ORIENTED_EDGE('',*,*,#21505,.F.);
#30389=ORIENTED_EDGE('',*,*,#21501,.F.);
#30390=ORIENTED_EDGE('',*,*,#21527,.F.);
#30391=ORIENTED_EDGE('',*,*,#21521,.F.);
#30392=ORIENTED_EDGE('',*,*,#21517,.F.);
#30393=ORIENTED_EDGE('',*,*,#21528,.F.);
#30394=ORIENTED_EDGE('',*,*,#21504,.F.);
#30395=ORIENTED_EDGE('',*,*,#21523,.T.);
#30396=ORIENTED_EDGE('',*,*,#21508,.F.);
#30397=ORIENTED_EDGE('',*,*,#21506,.F.);
#30398=ORIENTED_EDGE('',*,*,#21472,.F.);
#30399=ORIENTED_EDGE('',*,*,#21481,.T.);
#30400=ORIENTED_EDGE('',*,*,#21497,.F.);
#30401=ORIENTED_EDGE('',*,*,#21468,.F.);
#30402=ORIENTED_EDGE('',*,*,#21342,.F.);
#30403=ORIENTED_EDGE('',*,*,#21345,.F.);
#30404=ORIENTED_EDGE('',*,*,#21529,.T.);
#30405=ORIENTED_EDGE('',*,*,#21447,.F.);
#30406=ORIENTED_EDGE('',*,*,#21431,.F.);
#30407=ORIENTED_EDGE('',*,*,#21350,.F.);
#30408=ORIENTED_EDGE('',*,*,#21294,.F.);
#30409=ORIENTED_EDGE('',*,*,#21340,.F.);
#30410=ORIENTED_EDGE('',*,*,#21332,.F.);
#30411=ORIENTED_EDGE('',*,*,#21445,.F.);
#30412=ORIENTED_EDGE('',*,*,#21529,.F.);
#30413=ORIENTED_EDGE('',*,*,#21344,.F.);
#30414=ORIENTED_EDGE('',*,*,#21282,.F.);
#30415=ORIENTED_EDGE('',*,*,#21450,.F.);
#30416=ORIENTED_EDGE('',*,*,#21451,.F.);
#30417=ORIENTED_EDGE('',*,*,#21249,.T.);
#30418=ORIENTED_EDGE('',*,*,#21254,.F.);
#30419=ORIENTED_EDGE('',*,*,#21297,.F.);
#30420=ORIENTED_EDGE('',*,*,#21290,.F.);
#30421=ORIENTED_EDGE('',*,*,#21276,.F.);
#30422=ORIENTED_EDGE('',*,*,#21263,.F.);
#30423=ORIENTED_EDGE('',*,*,#21307,.T.);
#30424=ORIENTED_EDGE('',*,*,#21315,.T.);
#30425=ORIENTED_EDGE('',*,*,#21298,.F.);
#30426=ORIENTED_EDGE('',*,*,#21239,.F.);
#30427=ORIENTED_EDGE('',*,*,#21237,.F.);
#30428=ORIENTED_EDGE('',*,*,#21225,.T.);
#30429=ORIENTED_EDGE('',*,*,#21235,.F.);
#30430=ORIENTED_EDGE('',*,*,#21305,.T.);
#30431=ORIENTED_EDGE('',*,*,#21525,.T.);
#32061=CONICAL_SURFACE('',#37042,19.8,1.20210042413685);
#32062=CONICAL_SURFACE('',#37052,13.,0.785398163397448);
#32063=CONICAL_SURFACE('',#37059,13.,0.785398163397448);
#32064=CONICAL_SURFACE('',#37064,19.8,1.20210042413685);
#32065=CONICAL_SURFACE('',#37068,19.8,1.20210042413685);
#32066=CONICAL_SURFACE('',#37074,19.8,1.20210042413685);
#32067=CONICAL_SURFACE('',#37091,13.,0.785398163397448);
#32068=CONICAL_SURFACE('',#37096,19.8,1.20210042413685);
#32069=CONICAL_SURFACE('',#37108,13.,0.785398163397446);
#32070=CONICAL_SURFACE('',#37121,13.,0.785398163397448);
#32071=CONICAL_SURFACE('',#37123,13.,0.785398163397448);
#32072=CONICAL_SURFACE('',#37127,13.,0.785398163397448);
#32073=CONICAL_SURFACE('',#37129,13.,0.785398163397448);
#32074=CONICAL_SURFACE('',#37140,13.,0.785398163397448);
#32075=CONICAL_SURFACE('',#37145,19.8,1.20210042413685);
#32076=CONICAL_SURFACE('',#37154,13.,0.785398163397448);
#32077=CONICAL_SURFACE('',#37157,13.,0.785398163397448);
#32078=CONICAL_SURFACE('',#37161,13.,0.785398163397448);
#32079=CONICAL_SURFACE('',#37171,19.8,1.20210042413685);
#32080=CONICAL_SURFACE('',#37173,13.075,0.74837804752352);
#33784=ADVANCED_FACE('',(#4810),#2698,.T.);
#33785=ADVANCED_FACE('',(#4811),#2699,.T.);
#33786=ADVANCED_FACE('',(#4812),#32061,.T.);
#33787=ADVANCED_FACE('',(#4813),#2700,.F.);
#33788=ADVANCED_FACE('',(#4814),#2701,.T.);
#33789=ADVANCED_FACE('',(#4815),#2702,.T.);
#33790=ADVANCED_FACE('',(#4816),#2703,.T.);
#33791=ADVANCED_FACE('',(#4817),#2704,.F.);
#33792=ADVANCED_FACE('',(#4818),#2705,.F.);
#33793=ADVANCED_FACE('',(#4819),#2706,.T.);
#33794=ADVANCED_FACE('',(#4820),#2707,.T.);
#33795=ADVANCED_FACE('',(#4821),#32062,.F.);
#33796=ADVANCED_FACE('',(#4822),#2708,.T.);
#33797=ADVANCED_FACE('',(#4823),#2709,.T.);
#33798=ADVANCED_FACE('',(#4824),#2710,.T.);
#33799=ADVANCED_FACE('',(#4825),#2711,.T.);
#33800=ADVANCED_FACE('',(#4826),#2712,.T.);
#33801=ADVANCED_FACE('',(#4827),#32063,.F.);
#33802=ADVANCED_FACE('',(#4828),#2713,.T.);
#33803=ADVANCED_FACE('',(#4829),#32064,.T.);
#33804=ADVANCED_FACE('',(#4830),#2714,.T.);
#33805=ADVANCED_FACE('',(#4831),#2715,.T.);
#33806=ADVANCED_FACE('',(#4832),#2716,.T.);
#33807=ADVANCED_FACE('',(#4833),#32065,.T.);
#33808=ADVANCED_FACE('',(#4834),#2717,.T.);
#33809=ADVANCED_FACE('',(#4835),#2718,.T.);
#33810=ADVANCED_FACE('',(#4836),#32066,.T.);
#33811=ADVANCED_FACE('',(#4837),#2719,.F.);
#33812=ADVANCED_FACE('',(#4838),#2720,.T.);
#33813=ADVANCED_FACE('',(#4839),#2721,.T.);
#33814=ADVANCED_FACE('',(#4840),#2722,.T.);
#33815=ADVANCED_FACE('',(#4841),#2723,.T.);
#33816=ADVANCED_FACE('',(#4842),#2724,.T.);
#33817=ADVANCED_FACE('',(#4843),#2725,.T.);
#33818=ADVANCED_FACE('',(#4844),#2726,.T.);
#33819=ADVANCED_FACE('',(#4845),#2727,.T.);
#33820=ADVANCED_FACE('',(#4846),#2728,.T.);
#33821=ADVANCED_FACE('',(#4847),#2729,.T.);
#33822=ADVANCED_FACE('',(#4848),#2730,.F.);
#33823=ADVANCED_FACE('',(#4849),#2731,.F.);
#33824=ADVANCED_FACE('',(#4850),#2732,.T.);
#33825=ADVANCED_FACE('',(#4851),#2733,.T.);
#33826=ADVANCED_FACE('',(#4852),#32067,.F.);
#33827=ADVANCED_FACE('',(#4853),#2734,.T.);
#33828=ADVANCED_FACE('',(#4854),#2735,.T.);
#33829=ADVANCED_FACE('',(#4855),#2736,.T.);
#33830=ADVANCED_FACE('',(#4856),#32068,.T.);
#33831=ADVANCED_FACE('',(#4857),#2737,.F.);
#33832=ADVANCED_FACE('',(#4858),#2738,.F.);
#33833=ADVANCED_FACE('',(#4859),#2739,.T.);
#33834=ADVANCED_FACE('',(#4860),#2740,.T.);
#33835=ADVANCED_FACE('',(#4861),#2741,.T.);
#33836=ADVANCED_FACE('',(#4862),#2742,.F.);
#33837=ADVANCED_FACE('',(#4863),#2743,.T.);
#33838=ADVANCED_FACE('',(#4864),#2744,.F.);
#33839=ADVANCED_FACE('',(#4865),#2745,.T.);
#33840=ADVANCED_FACE('',(#4866),#32069,.F.);
#33841=ADVANCED_FACE('',(#4867),#2746,.T.);
#33842=ADVANCED_FACE('',(#4868),#2747,.T.);
#33843=ADVANCED_FACE('',(#4869),#2748,.T.);
#33844=ADVANCED_FACE('',(#4870),#2749,.T.);
#33845=ADVANCED_FACE('',(#4871),#2750,.T.);
#33846=ADVANCED_FACE('',(#4872),#2751,.T.);
#33847=ADVANCED_FACE('',(#4873),#2752,.T.);
#33848=ADVANCED_FACE('',(#4874),#2753,.T.);
#33849=ADVANCED_FACE('',(#4875),#2754,.T.);
#33850=ADVANCED_FACE('',(#4876),#2755,.T.);
#33851=ADVANCED_FACE('',(#4877),#32070,.F.);
#33852=ADVANCED_FACE('',(#4878),#32071,.F.);
#33853=ADVANCED_FACE('',(#4879),#2756,.T.);
#33854=ADVANCED_FACE('',(#4880),#32072,.F.);
#33855=ADVANCED_FACE('',(#4881),#32073,.F.);
#33856=ADVANCED_FACE('',(#4882),#2757,.T.);
#33857=ADVANCED_FACE('',(#4883),#3070,.F.);
#33858=ADVANCED_FACE('',(#4884),#32074,.F.);
#33859=ADVANCED_FACE('',(#4885),#2758,.T.);
#33860=ADVANCED_FACE('',(#4886),#2759,.T.);
#33861=ADVANCED_FACE('',(#4887),#2760,.T.);
#33862=ADVANCED_FACE('',(#4888),#32075,.T.);
#33863=ADVANCED_FACE('',(#4889),#2761,.T.);
#33864=ADVANCED_FACE('',(#4890),#2762,.T.);
#33865=ADVANCED_FACE('',(#4891),#2763,.T.);
#33866=ADVANCED_FACE('',(#4892),#2764,.T.);
#33867=ADVANCED_FACE('',(#4893),#2765,.T.);
#33868=ADVANCED_FACE('',(#4894),#2766,.T.);
#33869=ADVANCED_FACE('',(#4895),#2767,.T.);
#33870=ADVANCED_FACE('',(#4896),#32076,.F.);
#33871=ADVANCED_FACE('',(#4897),#2768,.T.);
#33872=ADVANCED_FACE('',(#4898),#32077,.F.);
#33873=ADVANCED_FACE('',(#4899),#2769,.T.);
#33874=ADVANCED_FACE('',(#4900),#2770,.T.);
#33875=ADVANCED_FACE('',(#4901),#32078,.F.);
#33876=ADVANCED_FACE('',(#4902),#2771,.F.);
#33877=ADVANCED_FACE('',(#4903),#2772,.F.);
#33878=ADVANCED_FACE('',(#4904),#2773,.T.);
#33879=ADVANCED_FACE('',(#4905),#2774,.T.);
#33880=ADVANCED_FACE('',(#4906),#2775,.T.);
#33881=ADVANCED_FACE('',(#4907),#2776,.T.);
#33882=ADVANCED_FACE('',(#4908),#2777,.T.);
#33883=ADVANCED_FACE('',(#4909),#2778,.T.);
#33884=ADVANCED_FACE('',(#4910),#32079,.T.);
#33885=ADVANCED_FACE('',(#4911),#32080,.F.);
#33886=ADVANCED_FACE('',(#4912),#2779,.F.);
#33887=ADVANCED_FACE('',(#4913),#2780,.F.);
#33888=ADVANCED_FACE('',(#4914),#2781,.F.);
#33889=ADVANCED_FACE('',(#4915),#2782,.T.);
#33890=ADVANCED_FACE('',(#4916),#2783,.T.);
#33891=ADVANCED_FACE('',(#4917),#2784,.F.);
#33892=ADVANCED_FACE('',(#4918),#2785,.F.);
#33893=ADVANCED_FACE('',(#4919),#2786,.F.);
#33894=ADVANCED_FACE('',(#4920),#2787,.T.);
#33895=ADVANCED_FACE('',(#4921,#1292),#2788,.F.);
#34216=CLOSED_SHELL('',(#33784,#33785,#33786,#33787,#33788,#33789,#33790,
#33791,#33792,#33793,#33794,#33795,#33796,#33797,#33798,#33799,#33800,#33801,
#33802,#33803,#33804,#33805,#33806,#33807,#33808,#33809,#33810,#33811,#33812,
#33813,#33814,#33815,#33816,#33817,#33818,#33819,#33820,#33821,#33822,#33823,
#33824,#33825,#33826,#33827,#33828,#33829,#33830,#33831,#33832,#33833,#33834,
#33835,#33836,#33837,#33838,#33839,#33840,#33841,#33842,#33843,#33844,#33845,
#33846,#33847,#33848,#33849,#33850,#33851,#33852,#33853,#33854,#33855,#33856,
#33857,#33858,#33859,#33860,#33861,#33862,#33863,#33864,#33865,#33866,#33867,
#33868,#33869,#33870,#33871,#33872,#33873,#33874,#33875,#33876,#33877,#33878,
#33879,#33880,#33881,#33882,#33883,#33884,#33885,#33886,#33887,#33888,#33889,
#33890,#33891,#33892,#33893,#33894,#33895));
#37037=AXIS2_PLACEMENT_3D('',#61978,#45453,#45454);
#37038=AXIS2_PLACEMENT_3D('',#61979,#45455,#45456);
#37039=AXIS2_PLACEMENT_3D('',#61994,#45460,#45461);
#37040=AXIS2_PLACEMENT_3D('',#61996,#45462,#45463);
#37041=AXIS2_PLACEMENT_3D('',#61999,#45465,#45466);
#37042=AXIS2_PLACEMENT_3D('',#62000,#45467,#45468);
#37043=AXIS2_PLACEMENT_3D('',#62024,#45469,#45470);
#37044=AXIS2_PLACEMENT_3D('',#62036,#45475,#45476);
#37045=AXIS2_PLACEMENT_3D('',#62040,#45479,#45480);
#37046=AXIS2_PLACEMENT_3D('',#62046,#45484,#45485);
#37047=AXIS2_PLACEMENT_3D('',#62056,#45491,#45492);
#37048=AXIS2_PLACEMENT_3D('',#62066,#45496,#45497);
#37049=AXIS2_PLACEMENT_3D('',#62071,#45500,#45501);
#37050=AXIS2_PLACEMENT_3D('',#62072,#45502,#45503);
#37051=AXIS2_PLACEMENT_3D('',#62080,#45508,#45509);
#37052=AXIS2_PLACEMENT_3D('',#62086,#45511,#45512);
#37053=AXIS2_PLACEMENT_3D('',#62093,#45513,#45514);
#37054=AXIS2_PLACEMENT_3D('',#62098,#45515,#45516);
#37055=AXIS2_PLACEMENT_3D('',#62111,#45521,#45522);
#37056=AXIS2_PLACEMENT_3D('',#62129,#45528,#45529);
#37057=AXIS2_PLACEMENT_3D('',#62137,#45534,#45535);
#37058=AXIS2_PLACEMENT_3D('',#62140,#45538,#45539);
#37059=AXIS2_PLACEMENT_3D('',#62155,#45543,#45544);
#37060=AXIS2_PLACEMENT_3D('',#62157,#45545,#45546);
#37061=AXIS2_PLACEMENT_3D('',#62168,#45547,#45548);
#37062=AXIS2_PLACEMENT_3D('',#62173,#45549,#45550);
#37063=AXIS2_PLACEMENT_3D('',#62175,#45551,#45552);
#37064=AXIS2_PLACEMENT_3D('',#62177,#45554,#45555);
#37065=AXIS2_PLACEMENT_3D('',#62201,#45556,#45557);
#37066=AXIS2_PLACEMENT_3D('',#62204,#45560,#45561);
#37067=AXIS2_PLACEMENT_3D('',#62212,#45564,#45565);
#37068=AXIS2_PLACEMENT_3D('',#62222,#45569,#45570);
#37069=AXIS2_PLACEMENT_3D('',#62224,#45571,#45572);
#37070=AXIS2_PLACEMENT_3D('',#62260,#45574,#45575);
#37071=AXIS2_PLACEMENT_3D('',#62275,#45579,#45580);
#37072=AXIS2_PLACEMENT_3D('',#62277,#45581,#45582);
#37073=AXIS2_PLACEMENT_3D('',#62280,#45584,#45585);
#37074=AXIS2_PLACEMENT_3D('',#62281,#45586,#45587);
#37075=AXIS2_PLACEMENT_3D('',#62305,#45588,#45589);
#37076=AXIS2_PLACEMENT_3D('',#62317,#45594,#45595);
#37077=AXIS2_PLACEMENT_3D('',#62321,#45598,#45599);
#37078=AXIS2_PLACEMENT_3D('',#62327,#45603,#45604);
#37079=AXIS2_PLACEMENT_3D('',#62330,#45607,#45608);
#37080=AXIS2_PLACEMENT_3D('',#62334,#45611,#45612);
#37081=AXIS2_PLACEMENT_3D('',#62338,#45615,#45616);
#37082=AXIS2_PLACEMENT_3D('',#62340,#45618,#45619);
#37083=AXIS2_PLACEMENT_3D('',#62346,#45623,#45624);
#37084=AXIS2_PLACEMENT_3D('',#62350,#45627,#45628);
#37085=AXIS2_PLACEMENT_3D('',#62354,#45631,#45632);
#37086=AXIS2_PLACEMENT_3D('',#62362,#45637,#45638);
#37087=AXIS2_PLACEMENT_3D('',#62372,#45642,#45643);
#37088=AXIS2_PLACEMENT_3D('',#62377,#45646,#45647);
#37089=AXIS2_PLACEMENT_3D('',#62378,#45648,#45649);
#37090=AXIS2_PLACEMENT_3D('',#62386,#45654,#45655);
#37091=AXIS2_PLACEMENT_3D('',#62392,#45657,#45658);
#37092=AXIS2_PLACEMENT_3D('',#62399,#45659,#45660);
#37093=AXIS2_PLACEMENT_3D('',#62404,#45661,#45662);
#37094=AXIS2_PLACEMENT_3D('',#62414,#45668,#45669);
#37095=AXIS2_PLACEMENT_3D('',#62418,#45672,#45673);
#37096=AXIS2_PLACEMENT_3D('',#62424,#45675,#45676);
#37097=AXIS2_PLACEMENT_3D('',#62434,#45677,#45678);
#37098=AXIS2_PLACEMENT_3D('',#62446,#45679,#45680);
#37099=AXIS2_PLACEMENT_3D('',#62456,#45684,#45685);
#37100=AXIS2_PLACEMENT_3D('',#62457,#45686,#45687);
#37101=AXIS2_PLACEMENT_3D('',#62458,#45688,#45689);
#37102=AXIS2_PLACEMENT_3D('',#62472,#45695,#45696);
#37103=AXIS2_PLACEMENT_3D('',#62478,#45700,#45701);
#37104=AXIS2_PLACEMENT_3D('',#62484,#45703,#45704);
#37105=AXIS2_PLACEMENT_3D('',#62498,#45708,#45709);
#37106=AXIS2_PLACEMENT_3D('',#62500,#45711,#45712);
#37107=AXIS2_PLACEMENT_3D('',#62510,#45716,#45717);
#37108=AXIS2_PLACEMENT_3D('',#62518,#45720,#45721);
#37109=AXIS2_PLACEMENT_3D('',#62520,#45722,#45723);
#37110=AXIS2_PLACEMENT_3D('',#62526,#45724,#45725);
#37111=AXIS2_PLACEMENT_3D('',#62530,#45726,#45727);
#37112=AXIS2_PLACEMENT_3D('',#62532,#45729,#45730);
#37113=AXIS2_PLACEMENT_3D('',#62535,#45733,#45734);
#37114=AXIS2_PLACEMENT_3D('',#62536,#45735,#45736);
#37115=AXIS2_PLACEMENT_3D('',#62543,#45738,#45739);
#37116=AXIS2_PLACEMENT_3D('',#62550,#45741,#45742);
#37117=AXIS2_PLACEMENT_3D('',#62557,#45744,#45745);
#37118=AXIS2_PLACEMENT_3D('',#62566,#45748,#45749);
#37119=AXIS2_PLACEMENT_3D('',#62573,#45751,#45752);
#37120=AXIS2_PLACEMENT_3D('',#62580,#45754,#45755);
#37121=AXIS2_PLACEMENT_3D('',#62596,#45759,#45760);
#37122=AXIS2_PLACEMENT_3D('',#62600,#45761,#45762);
#37123=AXIS2_PLACEMENT_3D('',#62601,#45763,#45764);
#37124=AXIS2_PLACEMENT_3D('',#62603,#45765,#45766);
#37125=AXIS2_PLACEMENT_3D('',#62604,#45767,#45768);
#37126=AXIS2_PLACEMENT_3D('',#62608,#45769,#45770);
#37127=AXIS2_PLACEMENT_3D('',#62617,#45773,#45774);
#37128=AXIS2_PLACEMENT_3D('',#62621,#45775,#45776);
#37129=AXIS2_PLACEMENT_3D('',#62622,#45777,#45778);
#37130=AXIS2_PLACEMENT_3D('',#62623,#45779,#45780);
#37131=AXIS2_PLACEMENT_3D('',#62624,#45781,#45782);
#37132=AXIS2_PLACEMENT_3D('',#62631,#45784,#45785);
#37133=AXIS2_PLACEMENT_3D('',#62633,#45786,#45787);
#37134=AXIS2_PLACEMENT_3D('',#62637,#45789,#45790);
#37135=AXIS2_PLACEMENT_3D('',#62641,#45792,#45793);
#37136=AXIS2_PLACEMENT_3D('',#62645,#45795,#45796);
#37137=AXIS2_PLACEMENT_3D('',#62649,#45798,#45799);
#37138=AXIS2_PLACEMENT_3D('',#62650,#45800,#45801);
#37139=AXIS2_PLACEMENT_3D('',#62651,#45802,#45803);
#37140=AXIS2_PLACEMENT_3D('',#62652,#45804,#45805);
#37141=AXIS2_PLACEMENT_3D('',#62659,#45806,#45807);
#37142=AXIS2_PLACEMENT_3D('',#62663,#45808,#45809);
#37143=AXIS2_PLACEMENT_3D('',#62671,#45812,#45813);
#37144=AXIS2_PLACEMENT_3D('',#62679,#45816,#45817);
#37145=AXIS2_PLACEMENT_3D('',#62681,#45819,#45820);
#37146=AXIS2_PLACEMENT_3D('',#62698,#45821,#45822);
#37147=AXIS2_PLACEMENT_3D('',#62702,#45823,#45824);
#37148=AXIS2_PLACEMENT_3D('',#62708,#45828,#45829);
#37149=AXIS2_PLACEMENT_3D('',#62715,#45832,#45833);
#37150=AXIS2_PLACEMENT_3D('',#62723,#45836,#45837);
#37151=AXIS2_PLACEMENT_3D('',#62730,#45839,#45840);
#37152=AXIS2_PLACEMENT_3D('',#62734,#45843,#45844);
#37153=AXIS2_PLACEMENT_3D('',#62737,#45847,#45848);
#37154=AXIS2_PLACEMENT_3D('',#62744,#45850,#45851);
#37155=AXIS2_PLACEMENT_3D('',#62750,#45852,#45853);
#37156=AXIS2_PLACEMENT_3D('',#62754,#45854,#45855);
#37157=AXIS2_PLACEMENT_3D('',#62762,#45858,#45859);
#37158=AXIS2_PLACEMENT_3D('',#62763,#45860,#45861);
#37159=AXIS2_PLACEMENT_3D('',#62764,#45862,#45863);
#37160=AXIS2_PLACEMENT_3D('',#62770,#45865,#45866);
#37161=AXIS2_PLACEMENT_3D('',#62775,#45867,#45868);
#37162=AXIS2_PLACEMENT_3D('',#62776,#45869,#45870);
#37163=AXIS2_PLACEMENT_3D('',#62777,#45871,#45872);
#37164=AXIS2_PLACEMENT_3D('',#62778,#45873,#45874);
#37165=AXIS2_PLACEMENT_3D('',#62779,#45875,#45876);
#37166=AXIS2_PLACEMENT_3D('',#62787,#45879,#45880);
#37167=AXIS2_PLACEMENT_3D('',#62792,#45884,#45885);
#37168=AXIS2_PLACEMENT_3D('',#62796,#45888,#45889);
#37169=AXIS2_PLACEMENT_3D('',#62800,#45892,#45893);
#37170=AXIS2_PLACEMENT_3D('',#62804,#45896,#45897);
#37171=AXIS2_PLACEMENT_3D('',#62805,#45898,#45899);
#37172=AXIS2_PLACEMENT_3D('',#62806,#45900,#45901);
#37173=AXIS2_PLACEMENT_3D('',#62810,#45902,#45903);
#37174=AXIS2_PLACEMENT_3D('',#62812,#45904,#45905);
#37175=AXIS2_PLACEMENT_3D('',#62814,#45907,#45908);
#37176=AXIS2_PLACEMENT_3D('',#62816,#45910,#45911);
#37177=AXIS2_PLACEMENT_3D('',#62818,#45913,#45914);
#37178=AXIS2_PLACEMENT_3D('',#62819,#45915,#45916);
#37179=AXIS2_PLACEMENT_3D('',#62820,#45917,#45918);
#37180=AXIS2_PLACEMENT_3D('',#62821,#45919,#45920);
#37181=AXIS2_PLACEMENT_3D('',#62823,#45922,#45923);
#37182=AXIS2_PLACEMENT_3D('',#62824,#45924,#45925);
#37183=AXIS2_PLACEMENT_3D('',#62825,#45926,#45927);
#37184=AXIS2_PLACEMENT_3D('',#62826,#45928,#45929);
#45453=DIRECTION('axis',(0.,0.,1.));
#45454=DIRECTION('refdir',(1.,0.,0.));
#45455=DIRECTION('center_axis',(0.707106781186547,0.353553390593274,0.612372435695795));
#45456=DIRECTION('ref_axis',(0.654653670707978,0.,-0.755928946018454));
#45457=DIRECTION('',(0.,0.866025403784439,-0.5));
#45458=DIRECTION('',(-0.532735444826016,-0.303096428117156,0.790142709318164));
#45459=DIRECTION('',(0.,-0.866025403784439,0.5));
#45460=DIRECTION('center_axis',(1.,0.,0.));
#45461=DIRECTION('ref_axis',(0.,0.,-1.));
#45462=DIRECTION('center_axis',(1.,0.,0.));
#45463=DIRECTION('ref_axis',(0.,1.,0.));
#45464=DIRECTION('',(0.,-0.866025403784439,-0.5));
#45465=DIRECTION('center_axis',(1.,0.,0.));
#45466=DIRECTION('ref_axis',(0.,0.,-1.));
#45467=DIRECTION('center_axis',(-1.,0.,0.));
#45468=DIRECTION('ref_axis',(0.,-1.,1.22464679914735E-16));
#45469=DIRECTION('center_axis',(0.,-0.5,-0.866025403784439));
#45470=DIRECTION('ref_axis',(0.,-0.866025403784439,0.5));
#45471=DIRECTION('',(1.,0.,0.));
#45472=DIRECTION('',(0.,-0.866025403784439,0.5));
#45473=DIRECTION('',(-0.654653670707977,-0.654653670707977,0.377964473009227));
#45474=DIRECTION('',(-1.,0.,0.));
#45475=DIRECTION('center_axis',(0.,-0.5,0.866025403784438));
#45476=DIRECTION('ref_axis',(1.,0.,0.));
#45477=DIRECTION('',(0.654653670707977,0.654653670707977,0.377964473009228));
#45478=DIRECTION('',(1.,0.,0.));
#45479=DIRECTION('center_axis',(0.,-0.500000000000004,-0.866025403784436));
#45480=DIRECTION('ref_axis',(-1.,0.,0.));
#45481=DIRECTION('',(1.,0.,0.));
#45482=DIRECTION('',(-1.,0.,0.));
#45483=DIRECTION('',(0.654653670707977,0.654653670707975,-0.377964473009231));
#45484=DIRECTION('center_axis',(0.707106781186548,-0.707106781186548,-1.49012597864166E-16));
#45485=DIRECTION('ref_axis',(-2.10735636863952E-16,0.,-1.));
#45486=DIRECTION('',(0.,2.10735636863952E-16,-1.));
#45487=DIRECTION('',(0.447213595499958,0.447213595499958,-0.774596669241483));
#45488=DIRECTION('',(0.654653670707976,0.654653670707976,0.37796447300923));
#45489=DIRECTION('',(0.,-2.10735636863952E-16,1.));
#45490=DIRECTION('',(-0.654653670707977,-0.654653670707977,-0.377964473009227));
#45491=DIRECTION('center_axis',(0.,-0.5,0.866025403784439));
#45492=DIRECTION('ref_axis',(0.,0.866025403784439,0.5));
#45493=DIRECTION('',(0.,0.866025403784439,0.5));
#45494=DIRECTION('',(-1.,0.,0.));
#45495=DIRECTION('',(0.,0.866025403784439,0.5));
#45496=DIRECTION('center_axis',(-1.,0.,0.));
#45497=DIRECTION('ref_axis',(0.,-0.866025403784439,-0.5));
#45498=DIRECTION('',(0.,-0.866025403784439,0.5));
#45499=DIRECTION('',(0.,-0.866025403784439,-0.5));
#45500=DIRECTION('center_axis',(1.,0.,0.));
#45501=DIRECTION('ref_axis',(0.,0.,-1.));
#45502=DIRECTION('center_axis',(0.707106781186549,-0.353553390593273,-0.612372435695793));
#45503=DIRECTION('ref_axis',(-0.654653670707976,0.,-0.755928946018456));
#45504=DIRECTION('',(-0.447213595499956,0.447213595499958,-0.774596669241484));
#45505=DIRECTION('',(0.,0.866025403784439,-0.5));
#45506=DIRECTION('',(-0.654653670707975,-3.35699888340127E-15,-0.755928946018457));
#45507=DIRECTION('',(0.654653670707976,0.654653670707978,0.377964473009228));
#45508=DIRECTION('center_axis',(0.707106781186546,0.353553390593274,-0.612372435695796));
#45509=DIRECTION('ref_axis',(-0.654653670707979,0.,-0.755928946018453));
#45510=DIRECTION('',(0.532735444826017,0.303096428117156,0.790142709318163));
#45511=DIRECTION('center_axis',(1.,0.,0.));
#45512=DIRECTION('ref_axis',(0.,0.,-1.));
#45513=DIRECTION('center_axis',(-1.,0.,0.));
#45514=DIRECTION('ref_axis',(0.,0.,-1.));
#45515=DIRECTION('center_axis',(0.,-0.866025403784437,0.500000000000003));
#45516=DIRECTION('ref_axis',(1.,0.,0.));
#45517=DIRECTION('',(-0.447213595499955,0.447213595499962,0.774596669241483));
#45518=DIRECTION('',(-1.,0.,0.));
#45519=DIRECTION('',(1.,0.,0.));
#45520=DIRECTION('',(0.44721359549996,0.44721359549996,0.774596669241481));
#45521=DIRECTION('center_axis',(0.,-0.5,0.866025403784439));
#45522=DIRECTION('ref_axis',(0.,-0.866025403784439,-0.5));
#45523=DIRECTION('',(0.,-0.866025403784439,-0.5));
#45524=DIRECTION('',(-1.,0.,0.));
#45525=DIRECTION('',(1.,0.,0.));
#45526=DIRECTION('',(0.,-0.866025403784439,-0.5));
#45527=DIRECTION('',(1.,0.,0.));
#45528=DIRECTION('center_axis',(0.707106781186549,-0.353553390593273,0.612372435695794));
#45529=DIRECTION('ref_axis',(0.654653670707976,0.,-0.755928946018455));
#45530=DIRECTION('',(-0.654653670707977,-0.654653670707977,0.377964473009228));
#45531=DIRECTION('',(0.,0.866025403784439,0.5));
#45532=DIRECTION('',(-0.654653670707976,-0.654653670707978,0.377964473009228));
#45533=DIRECTION('',(0.654653670707976,0.,-0.755928946018455));
#45534=DIRECTION('center_axis',(0.707106781186548,-0.707106781186548,-1.49012597864166E-16));
#45535=DIRECTION('ref_axis',(-2.10735636863952E-16,0.,-1.));
#45536=DIRECTION('',(0.,2.10735636863952E-16,-1.));
#45537=DIRECTION('',(0.,-2.10735636863952E-16,1.));
#45538=DIRECTION('center_axis',(0.707106781186547,-0.353553390593274,0.612372435695795));
#45539=DIRECTION('ref_axis',(0.654653670707978,0.,-0.755928946018454));
#45540=DIRECTION('',(0.,0.866025403784439,0.5));
#45541=DIRECTION('',(-0.532735444826014,-0.835831872943173,0.132582148113298));
#45542=DIRECTION('',(0.,-0.866025403784439,-0.5));
#45543=DIRECTION('center_axis',(1.,0.,0.));
#45544=DIRECTION('ref_axis',(0.,0.,-1.));
#45545=DIRECTION('center_axis',(1.,0.,0.));
#45546=DIRECTION('ref_axis',(0.,0.,-1.));
#45547=DIRECTION('center_axis',(-1.,0.,0.));
#45548=DIRECTION('ref_axis',(0.,0.,-1.));
#45549=DIRECTION('center_axis',(1.,0.,0.));
#45550=DIRECTION('ref_axis',(0.,0.,-1.));
#45551=DIRECTION('center_axis',(1.,0.,0.));
#45552=DIRECTION('ref_axis',(0.,1.,0.));
#45553=DIRECTION('',(0.,-1.22464679914735E-16,-1.));
#45554=DIRECTION('center_axis',(-1.,0.,0.));
#45555=DIRECTION('ref_axis',(0.,1.,0.));
#45556=DIRECTION('center_axis',(0.,-1.,0.));
#45557=DIRECTION('ref_axis',(0.,0.,-1.));
#45558=DIRECTION('',(1.,0.,0.));
#45559=DIRECTION('',(-1.,0.,0.));
#45560=DIRECTION('center_axis',(0.,-0.866025403784439,-0.5));
#45561=DIRECTION('ref_axis',(-1.,0.,0.));
#45562=DIRECTION('',(-1.,0.,0.));
#45563=DIRECTION('',(1.,0.,0.));
#45564=DIRECTION('center_axis',(0.,-0.5,-0.866025403784439));
#45565=DIRECTION('ref_axis',(0.,0.866025403784439,-0.5));
#45566=DIRECTION('',(-1.,0.,0.));
#45567=DIRECTION('',(0.,0.866025403784439,-0.5));
#45568=DIRECTION('',(-1.,0.,0.));
#45569=DIRECTION('center_axis',(1.,0.,0.));
#45570=DIRECTION('ref_axis',(0.,1.,0.));
#45571=DIRECTION('center_axis',(-1.,0.,0.));
#45572=DIRECTION('ref_axis',(0.,1.,0.));
#45573=DIRECTION('',(0.360399279202162,-0.932798134405597,-1.14234824955044E-16));
#45574=DIRECTION('center_axis',(0.707106781186547,-0.707106781186548,8.65956056235494E-17));
#45575=DIRECTION('ref_axis',(1.22464679914735E-16,0.,-1.));
#45576=DIRECTION('',(0.,1.22464679914735E-16,1.));
#45577=DIRECTION('',(-0.532735444826015,-0.532735444826014,-0.657560561204865));
#45578=DIRECTION('',(0.,-1.22464679914735E-16,-1.));
#45579=DIRECTION('center_axis',(1.,0.,0.));
#45580=DIRECTION('ref_axis',(0.,0.,-1.));
#45581=DIRECTION('center_axis',(1.,0.,0.));
#45582=DIRECTION('ref_axis',(0.,1.,0.));
#45583=DIRECTION('',(0.,0.866025403784438,-0.5));
#45584=DIRECTION('center_axis',(1.,0.,0.));
#45585=DIRECTION('ref_axis',(0.,0.,-1.));
#45586=DIRECTION('center_axis',(-1.,0.,0.));
#45587=DIRECTION('ref_axis',(0.,1.,0.));
#45588=DIRECTION('center_axis',(0.,1.,-1.22464679914735E-16));
#45589=DIRECTION('ref_axis',(0.,-1.22464679914735E-16,-1.));
#45590=DIRECTION('',(1.,0.,0.));
#45591=DIRECTION('',(0.,-1.22464679914735E-16,-1.));
#45592=DIRECTION('',(0.65465367070798,9.2574596412433E-17,0.755928946018452));
#45593=DIRECTION('',(-1.,0.,0.));
#45594=DIRECTION('center_axis',(0.,-0.499999999999999,-0.866025403784439));
#45595=DIRECTION('ref_axis',(-1.,0.,0.));
#45596=DIRECTION('',(1.,0.,0.));
#45597=DIRECTION('',(-0.654653670707979,0.654653670707976,-0.377964473009225));
#45598=DIRECTION('center_axis',(0.547750005235848,5.84175495892749E-17,
-0.836642057133233));
#45599=DIRECTION('ref_axis',(-0.836642057133233,0.,-0.547750005235848));
#45600=DIRECTION('',(0.,-1.,0.));
#45601=DIRECTION('',(-0.677497944020813,0.586730430533744,-0.443558268701259));
#45602=DIRECTION('',(0.677497944020809,0.586730430533752,0.443558268701256));
#45603=DIRECTION('center_axis',(0.707106781186545,0.353553390593275,-0.612372435695797));
#45604=DIRECTION('ref_axis',(-0.65465367070798,0.,-0.755928946018452));
#45605=DIRECTION('',(0.,-0.866025403784439,-0.5));
#45606=DIRECTION('',(0.,0.866025403784439,0.5));
#45607=DIRECTION('center_axis',(0.,0.500000000000003,-0.866025403784437));
#45608=DIRECTION('ref_axis',(-1.,0.,0.));
#45609=DIRECTION('',(1.,0.,0.));
#45610=DIRECTION('',(0.654653670707977,0.654653670707975,0.377964473009231));
#45611=DIRECTION('center_axis',(0.707106781186548,-0.353553390593274,-0.612372435695794));
#45612=DIRECTION('ref_axis',(-0.654653670707977,0.,-0.755928946018455));
#45613=DIRECTION('',(0.,-0.866025403784439,0.5));
#45614=DIRECTION('',(-0.654653670707977,-9.25745964124333E-17,-0.755928946018455));
#45615=DIRECTION('center_axis',(0.,0.,-1.));
#45616=DIRECTION('ref_axis',(-1.,0.,0.));
#45617=DIRECTION('',(1.,0.,0.));
#45618=DIRECTION('center_axis',(0.,0.5,-0.866025403784439));
#45619=DIRECTION('ref_axis',(0.,0.866025403784439,0.5));
#45620=DIRECTION('',(-1.,0.,0.));
#45621=DIRECTION('',(0.,0.866025403784439,0.5));
#45622=DIRECTION('',(-1.,0.,0.));
#45623=DIRECTION('center_axis',(0.707106781186547,0.707106781186548,-8.65956056235494E-17));
#45624=DIRECTION('ref_axis',(-1.22464679914735E-16,0.,-1.));
#45625=DIRECTION('',(0.,1.22464679914735E-16,1.));
#45626=DIRECTION('',(0.532735444826015,-0.532735444826015,0.657560561204864));
#45627=DIRECTION('center_axis',(0.,1.,0.));
#45628=DIRECTION('ref_axis',(0.,0.,1.));
#45629=DIRECTION('',(1.,0.,0.));
#45630=DIRECTION('',(0.654653670707976,0.,0.755928946018455));
#45631=DIRECTION('center_axis',(0.707106781186547,0.353553390593274,-0.612372435695795));
#45632=DIRECTION('ref_axis',(-0.654653670707978,0.,-0.755928946018454));
#45633=DIRECTION('',(0.447213595499961,0.447213595499955,0.774596669241484));
#45634=DIRECTION('',(0.654653670707978,-0.654653670707975,0.377964473009229));
#45635=DIRECTION('',(0.,-0.866025403784439,-0.5));
#45636=DIRECTION('',(-0.654653670707977,0.654653670707977,-0.377964473009227));
#45637=DIRECTION('center_axis',(0.,-0.5,-0.866025403784438));
#45638=DIRECTION('ref_axis',(0.,-0.866025403784438,0.5));
#45639=DIRECTION('',(0.,-0.866025403784438,0.5));
#45640=DIRECTION('',(-1.,0.,0.));
#45641=DIRECTION('',(0.,-0.866025403784438,0.5));
#45642=DIRECTION('center_axis',(-1.,0.,0.));
#45643=DIRECTION('ref_axis',(0.,0.866025403784438,-0.5));
#45644=DIRECTION('',(0.,-3.16103455295928E-16,-1.));
#45645=DIRECTION('',(0.,0.866025403784438,-0.5));
#45646=DIRECTION('center_axis',(1.,0.,0.));
#45647=DIRECTION('ref_axis',(0.,0.,-1.));
#45648=DIRECTION('center_axis',(0.707106781186546,0.707106781186549,-2.2351889679625E-16));
#45649=DIRECTION('ref_axis',(-3.1610345529593E-16,0.,-1.));
#45650=DIRECTION('',(-0.447213595499957,0.447213595499956,0.774596669241486));
#45651=DIRECTION('',(0.,3.16103455295928E-16,1.));
#45652=DIRECTION('',(-0.65465367070798,0.654653670707975,0.377964473009226));
#45653=DIRECTION('',(0.654653670707979,-0.654653670707976,0.377964473009227));
#45654=DIRECTION('center_axis',(0.707106781186547,0.353553390593275,0.612372435695795));
#45655=DIRECTION('ref_axis',(0.654653670707978,0.,-0.755928946018454));
#45656=DIRECTION('',(0.532735444826016,-0.835831872943172,-0.132582148113299));
#45657=DIRECTION('center_axis',(1.,0.,0.));
#45658=DIRECTION('ref_axis',(0.,0.,-1.));
#45659=DIRECTION('center_axis',(-1.,0.,0.));
#45660=DIRECTION('ref_axis',(0.,0.,-1.));
#45661=DIRECTION('center_axis',(0.707106781186549,-0.353553390593273,0.612372435695793));
#45662=DIRECTION('ref_axis',(0.654653670707976,0.,-0.755928946018456));
#45663=DIRECTION('',(-0.447213595499957,-0.894427190999917,0.));
#45664=DIRECTION('',(-0.654653670707977,-0.654653670707975,0.377964473009231));
#45665=DIRECTION('',(-0.654653670707976,0.,0.755928946018456));
#45666=DIRECTION('',(0.,0.866025403784439,0.5));
#45667=DIRECTION('',(-0.654653670707977,-2.93737402297611E-15,0.755928946018455));
#45668=DIRECTION('center_axis',(0.,0.,1.));
#45669=DIRECTION('ref_axis',(1.,0.,0.));
#45670=DIRECTION('',(-0.447213595499958,0.894427190999916,0.));
#45671=DIRECTION('',(-1.,0.,0.));
#45672=DIRECTION('center_axis',(0.,-1.,0.));
#45673=DIRECTION('ref_axis',(0.,0.,-1.));
#45674=DIRECTION('',(1.,0.,0.));
#45675=DIRECTION('center_axis',(-1.,0.,0.));
#45676=DIRECTION('ref_axis',(0.,1.,0.));
#45677=DIRECTION('center_axis',(1.,0.,0.));
#45678=DIRECTION('ref_axis',(0.,1.,0.));
#45679=DIRECTION('center_axis',(0.,0.5,0.866025403784439));
#45680=DIRECTION('ref_axis',(0.,0.866025403784439,-0.5));
#45681=DIRECTION('',(0.,0.866025403784439,-0.5));
#45682=DIRECTION('',(-1.,0.,0.));
#45683=DIRECTION('',(0.,0.866025403784439,-0.5));
#45684=DIRECTION('center_axis',(-1.,0.,0.));
#45685=DIRECTION('ref_axis',(0.,-0.866025403784439,0.5));
#45686=DIRECTION('center_axis',(1.,0.,0.));
#45687=DIRECTION('ref_axis',(0.,0.,1.));
#45688=DIRECTION('center_axis',(0.,0.5,0.866025403784439));
#45689=DIRECTION('ref_axis',(0.,-0.866025403784439,0.5));
#45690=DIRECTION('',(0.,-0.866025403784439,0.5));
#45691=DIRECTION('',(-1.,0.,0.));
#45692=DIRECTION('',(1.,0.,0.));
#45693=DIRECTION('',(0.,-0.866025403784439,0.5));
#45694=DIRECTION('',(1.,0.,0.));
#45695=DIRECTION('center_axis',(0.707106781186547,0.353553390593274,0.612372435695795));
#45696=DIRECTION('ref_axis',(0.654653670707978,0.,-0.755928946018454));
#45697=DIRECTION('',(0.,0.866025403784439,-0.5));
#45698=DIRECTION('',(0.654653670707978,0.,-0.755928946018454));
#45699=DIRECTION('',(-0.654653670707979,0.654653670707974,0.37796447300923));
#45700=DIRECTION('center_axis',(0.,-0.500000000000005,0.866025403784436));
#45701=DIRECTION('ref_axis',(1.,0.,0.));
#45702=DIRECTION('',(1.,0.,0.));
#45703=DIRECTION('center_axis',(0.,1.,0.));
#45704=DIRECTION('ref_axis',(0.,0.,-1.));
#45705=DIRECTION('',(0.,0.,-1.));
#45706=DIRECTION('',(-1.,0.,0.));
#45707=DIRECTION('',(0.,0.,-1.));
#45708=DIRECTION('center_axis',(0.,0.500000000000005,0.866025403784436));
#45709=DIRECTION('ref_axis',(1.,0.,0.));
#45710=DIRECTION('',(-1.,0.,0.));
#45711=DIRECTION('center_axis',(0.,-1.,0.));
#45712=DIRECTION('ref_axis',(0.,0.,1.));
#45713=DIRECTION('',(0.,0.,1.));
#45714=DIRECTION('',(1.,0.,0.));
#45715=DIRECTION('',(0.,0.,1.));
#45716=DIRECTION('center_axis',(0.707106781186547,0.707106781186548,0.));
#45717=DIRECTION('ref_axis',(0.,0.,-1.));
#45718=DIRECTION('',(0.,0.,-1.));
#45719=DIRECTION('',(-0.532735444826015,0.532735444826015,0.657560561204864));
#45720=DIRECTION('center_axis',(1.,0.,0.));
#45721=DIRECTION('ref_axis',(0.,0.,1.));
#45722=DIRECTION('center_axis',(1.,0.,0.));
#45723=DIRECTION('ref_axis',(0.,0.,1.));
#45724=DIRECTION('center_axis',(-1.,0.,0.));
#45725=DIRECTION('ref_axis',(0.,0.,1.));
#45726=DIRECTION('center_axis',(1.,0.,0.));
#45727=DIRECTION('ref_axis',(0.,0.,-1.));
#45728=DIRECTION('',(0.,-0.866025403784439,0.5));
#45729=DIRECTION('center_axis',(0.550547030005201,0.13078400442267,-0.824495913840465));
#45730=DIRECTION('ref_axis',(-0.831638955930086,0.,-0.555316708716312));
#45731=DIRECTION('',(0.,-0.987651911521988,-0.1566642960823));
#45732=DIRECTION('',(0.701026414838316,0.463839941019002,0.541677463823654));
#45733=DIRECTION('center_axis',(0.707106781186545,-0.353553390593275,-0.612372435695796));
#45734=DIRECTION('ref_axis',(-0.654653670707979,0.,-0.755928946018453));
#45735=DIRECTION('center_axis',(0.,0.1566642960823,-0.987651911521988));
#45736=DIRECTION('ref_axis',(-1.,0.,0.));
#45737=DIRECTION('',(1.,0.,0.));
#45738=DIRECTION('center_axis',(0.,0.933663793515453,0.358150695487714));
#45739=DIRECTION('ref_axis',(0.,-0.358150695487714,0.933663793515453));
#45740=DIRECTION('',(-1.,0.,0.));
#45741=DIRECTION('center_axis',(0.,0.933663793515453,-0.358150695487715));
#45742=DIRECTION('ref_axis',(0.,0.358150695487715,0.933663793515453));
#45743=DIRECTION('',(1.,0.,0.));
#45744=DIRECTION('center_axis',(0.,0.776999497433153,0.629501216034272));
#45745=DIRECTION('ref_axis',(1.,0.,0.));
#45746=DIRECTION('',(-1.,0.,0.));
#45747=DIRECTION('',(1.,0.,0.));
#45748=DIRECTION('center_axis',(0.,-0.776999497433154,0.629501216034272));
#45749=DIRECTION('ref_axis',(1.,0.,0.));
#45750=DIRECTION('',(-1.,0.,0.));
#45751=DIRECTION('center_axis',(0.,-0.156664296082299,0.987651911521989));
#45752=DIRECTION('ref_axis',(1.,0.,0.));
#45753=DIRECTION('',(1.,0.,0.));
#45754=DIRECTION('center_axis',(0.,-0.933663793515451,-0.358150695487721));
#45755=DIRECTION('ref_axis',(0.,0.358150695487721,-0.933663793515451));
#45756=DIRECTION('',(1.,0.,0.));
#45757=DIRECTION('',(0.532735444826014,-0.303096428117161,0.790142709318163));
#45758=DIRECTION('',(-1.,0.,0.));
#45759=DIRECTION('center_axis',(1.,0.,0.));
#45760=DIRECTION('ref_axis',(0.,0.,-1.));
#45761=DIRECTION('center_axis',(-1.,0.,0.));
#45762=DIRECTION('ref_axis',(0.,0.,-1.));
#45763=DIRECTION('center_axis',(1.,0.,0.));
#45764=DIRECTION('ref_axis',(0.,0.,-1.));
#45765=DIRECTION('center_axis',(1.,0.,0.));
#45766=DIRECTION('ref_axis',(0.,0.,-1.));
#45767=DIRECTION('center_axis',(-1.,0.,0.));
#45768=DIRECTION('ref_axis',(0.,0.,-1.));
#45769=DIRECTION('center_axis',(0.,0.156664296082297,0.987651911521989));
#45770=DIRECTION('ref_axis',(1.,0.,0.));
#45771=DIRECTION('',(-1.,0.,0.));
#45772=DIRECTION('',(1.,0.,0.));
#45773=DIRECTION('center_axis',(1.,0.,0.));
#45774=DIRECTION('ref_axis',(0.,0.,-1.));
#45775=DIRECTION('center_axis',(-1.,0.,0.));
#45776=DIRECTION('ref_axis',(0.,0.,-1.));
#45777=DIRECTION('center_axis',(1.,0.,0.));
#45778=DIRECTION('ref_axis',(0.,0.,1.));
#45779=DIRECTION('center_axis',(-1.,0.,0.));
#45780=DIRECTION('ref_axis',(0.,0.,1.));
#45781=DIRECTION('center_axis',(0.,0.776999497433153,-0.629501216034272));
#45782=DIRECTION('ref_axis',(-1.,0.,0.));
#45783=DIRECTION('',(-1.,0.,0.));
#45784=DIRECTION('center_axis',(1.,0.,0.));
#45785=DIRECTION('ref_axis',(0.,0.,-1.));
#45786=DIRECTION('center_axis',(-1.,0.,0.));
#45787=DIRECTION('ref_axis',(0.,0.,-1.));
#45788=DIRECTION('',(1.,0.,0.));
#45789=DIRECTION('center_axis',(-1.,0.,0.));
#45790=DIRECTION('ref_axis',(0.,0.,1.));
#45791=DIRECTION('',(-1.,0.,0.));
#45792=DIRECTION('center_axis',(-1.,0.,0.));
#45793=DIRECTION('ref_axis',(0.,0.,1.));
#45794=DIRECTION('',(1.,0.,0.));
#45795=DIRECTION('center_axis',(-1.,0.,0.));
#45796=DIRECTION('ref_axis',(0.,0.,1.));
#45797=DIRECTION('',(-1.,0.,0.));
#45798=DIRECTION('center_axis',(-1.,0.,0.));
#45799=DIRECTION('ref_axis',(0.,0.,-1.));
#45800=DIRECTION('center_axis',(-1.,0.,0.));
#45801=DIRECTION('ref_axis',(0.,0.,-1.));
#45802=DIRECTION('center_axis',(-1.,0.,0.));
#45803=DIRECTION('ref_axis',(0.,0.,1.));
#45804=DIRECTION('center_axis',(1.,0.,0.));
#45805=DIRECTION('ref_axis',(0.,0.,-1.));
#45806=DIRECTION('center_axis',(1.,0.,0.));
#45807=DIRECTION('ref_axis',(0.,0.,-1.));
#45808=DIRECTION('center_axis',(0.707106781186546,-0.353553390593275,-0.612372435695796));
#45809=DIRECTION('ref_axis',(-0.654653670707979,0.,-0.755928946018453));
#45810=DIRECTION('',(0.,0.866025403784438,-0.5));
#45811=DIRECTION('',(0.,-0.866025403784438,0.5));
#45812=DIRECTION('center_axis',(0.,0.5,-0.866025403784438));
#45813=DIRECTION('ref_axis',(-1.,0.,0.));
#45814=DIRECTION('',(1.,0.,0.));
#45815=DIRECTION('',(-1.,0.,0.));
#45816=DIRECTION('center_axis',(0.,0.86602540378444,-0.499999999999997));
#45817=DIRECTION('ref_axis',(0.,0.499999999999997,0.86602540378444));
#45818=DIRECTION('',(1.,0.,0.));
#45819=DIRECTION('center_axis',(-1.,0.,0.));
#45820=DIRECTION('ref_axis',(0.,1.,0.));
#45821=DIRECTION('center_axis',(1.,0.,0.));
#45822=DIRECTION('ref_axis',(0.,1.,0.));
#45823=DIRECTION('center_axis',(0.,1.,-3.16103455295928E-16));
#45824=DIRECTION('ref_axis',(0.,3.16103455295928E-16,1.));
#45825=DIRECTION('',(-1.,0.,0.));
#45826=DIRECTION('',(0.,3.16103455295928E-16,1.));
#45827=DIRECTION('',(-1.,0.,0.));
#45828=DIRECTION('center_axis',(0.550547030005203,-0.648642404490973,-0.525510227158919));
#45829=DIRECTION('ref_axis',(-0.690467539500804,0.,-0.723363378182574));
#45830=DIRECTION('',(0.,-0.629501216034272,0.776999497433153));
#45831=DIRECTION('',(0.701026414838314,0.701026414838313,-0.130858440300507));
#45832=DIRECTION('center_axis',(0.550547030005205,-0.130784004422669,-0.824495913840462));
#45833=DIRECTION('ref_axis',(-0.831638955930083,0.,-0.555316708716316));
#45834=DIRECTION('',(0.,-0.987651911521988,0.156664296082301));
#45835=DIRECTION('',(-0.701026414838315,0.463839941019,-0.541677463823657));
#45836=DIRECTION('center_axis',(0.,-0.156664296082301,-0.987651911521988));
#45837=DIRECTION('ref_axis',(-1.,0.,0.));
#45838=DIRECTION('',(1.,0.,0.));
#45839=DIRECTION('center_axis',(0.550547030005202,-0.77942640891364,0.298985686681551));
#45840=DIRECTION('ref_axis',(0.477236470436039,0.,-0.878774915029868));
#45841=DIRECTION('',(0.,0.358150695487721,0.93366379351545));
#45842=DIRECTION('',(0.701026414838314,0.237186473819303,-0.672535904124163));
#45843=DIRECTION('center_axis',(0.707106781186546,-0.353553390593274,0.612372435695796));
#45844=DIRECTION('ref_axis',(0.654653670707978,0.,-0.755928946018453));
#45845=DIRECTION('',(0.,-0.866025403784439,-0.499999999999999));
#45846=DIRECTION('',(0.,0.866025403784439,0.499999999999999));
#45847=DIRECTION('center_axis',(0.,-0.933663793515451,0.358150695487721));
#45848=DIRECTION('ref_axis',(0.,-0.358150695487721,-0.93366379351545));
#45849=DIRECTION('',(-1.,0.,0.));
#45850=DIRECTION('center_axis',(1.,0.,0.));
#45851=DIRECTION('ref_axis',(0.,0.,1.));
#45852=DIRECTION('center_axis',(1.,0.,0.));
#45853=DIRECTION('ref_axis',(0.,0.,1.));
#45854=DIRECTION('center_axis',(0.707106781186547,0.353553390593274,-0.612372435695795));
#45855=DIRECTION('ref_axis',(-0.654653670707978,0.,-0.755928946018454));
#45856=DIRECTION('',(0.,-0.866025403784439,-0.499999999999999));
#45857=DIRECTION('',(0.,0.866025403784439,0.499999999999999));
#45858=DIRECTION('center_axis',(1.,0.,0.));
#45859=DIRECTION('ref_axis',(0.,0.,1.));
#45860=DIRECTION('center_axis',(1.,0.,0.));
#45861=DIRECTION('ref_axis',(0.,0.,1.));
#45862=DIRECTION('center_axis',(0.707106781186547,-0.707106781186548,0.));
#45863=DIRECTION('ref_axis',(0.,0.,-1.));
#45864=DIRECTION('',(0.,0.,1.));
#45865=DIRECTION('center_axis',(0.,-0.776999497433153,-0.629501216034272));
#45866=DIRECTION('ref_axis',(-1.,0.,0.));
#45867=DIRECTION('center_axis',(1.,0.,0.));
#45868=DIRECTION('ref_axis',(0.,0.,1.));
#45869=DIRECTION('center_axis',(1.,0.,0.));
#45870=DIRECTION('ref_axis',(0.,0.,1.));
#45871=DIRECTION('center_axis',(0.,0.5,0.866025403784438));
#45872=DIRECTION('ref_axis',(0.,0.866025403784438,-0.5));
#45873=DIRECTION('center_axis',(-1.,0.,0.));
#45874=DIRECTION('ref_axis',(0.,0.,1.));
#45875=DIRECTION('center_axis',(0.,1.,4.44089209850062E-15));
#45876=DIRECTION('ref_axis',(0.,-4.44089209850062E-15,1.));
#45877=DIRECTION('',(-1.,0.,0.));
#45878=DIRECTION('',(-0.654653670707976,-3.35699888340126E-15,0.755928946018456));
#45879=DIRECTION('center_axis',(0.54775000523585,0.72455327535185,0.418321028566618));
#45880=DIRECTION('ref_axis',(0.60694953464716,0.,-0.794740374205058));
#45881=DIRECTION('',(0.,0.500000000000002,-0.866025403784437));
#45882=DIRECTION('',(-0.67749794402081,0.0907675134870587,0.729902592366236));
#45883=DIRECTION('',(0.677497944020809,-0.677497944020809,0.286344323664976));
#45884=DIRECTION('center_axis',(0.707106781186547,0.353553390593274,0.612372435695795));
#45885=DIRECTION('ref_axis',(0.654653670707978,0.,-0.755928946018454));
#45886=DIRECTION('',(0.,0.866025403784439,-0.5));
#45887=DIRECTION('',(0.654653670707978,-0.654653670707977,-0.377964473009226));
#45888=DIRECTION('center_axis',(0.,0.499999999999999,0.866025403784439));
#45889=DIRECTION('ref_axis',(1.,0.,0.));
#45890=DIRECTION('',(1.,0.,0.));
#45891=DIRECTION('',(0.654653670707977,-0.654653670707977,0.377964473009228));
#45892=DIRECTION('center_axis',(0.707106781186548,0.707106781186548,-2.2351889679625E-16));
#45893=DIRECTION('ref_axis',(-3.16103455295928E-16,0.,-1.));
#45894=DIRECTION('',(0.,-3.16103455295928E-16,-1.));
#45895=DIRECTION('',(-0.654653670707977,0.654653670707977,0.377964473009227));
#45896=DIRECTION('center_axis',(0.,0.866025403784437,0.500000000000002));
#45897=DIRECTION('ref_axis',(1.,0.,0.));
#45898=DIRECTION('center_axis',(-1.,0.,0.));
#45899=DIRECTION('ref_axis',(0.,1.,0.));
#45900=DIRECTION('center_axis',(1.,0.,0.));
#45901=DIRECTION('ref_axis',(0.,1.,0.));
#45902=DIRECTION('center_axis',(-1.,0.,0.));
#45903=DIRECTION('ref_axis',(0.,1.,0.));
#45904=DIRECTION('center_axis',(1.,0.,0.));
#45905=DIRECTION('ref_axis',(0.,1.,0.));
#45906=DIRECTION('',(0.732793491626298,0.680451099367279,8.33312260816436E-17));
#45907=DIRECTION('center_axis',(0.,0.499999999999999,-0.866025403784439));
#45908=DIRECTION('ref_axis',(0.,-0.866025403784439,-0.499999999999999));
#45909=DIRECTION('',(0.,-0.866025403784439,-0.499999999999999));
#45910=DIRECTION('center_axis',(0.,-0.499999999999999,0.866025403784439));
#45911=DIRECTION('ref_axis',(0.,0.866025403784439,0.499999999999999));
#45912=DIRECTION('',(0.,0.866025403784439,0.499999999999999));
#45913=DIRECTION('center_axis',(-1.,0.,0.));
#45914=DIRECTION('ref_axis',(0.,0.866025403784439,0.499999999999999));
#45915=DIRECTION('center_axis',(1.,0.,0.));
#45916=DIRECTION('ref_axis',(0.,0.,-1.));
#45917=DIRECTION('center_axis',(1.,0.,0.));
#45918=DIRECTION('ref_axis',(0.,0.,-1.));
#45919=DIRECTION('center_axis',(0.,-1.,1.22464679914735E-16));
#45920=DIRECTION('ref_axis',(0.,1.22464679914735E-16,1.));
#45921=DIRECTION('',(0.,1.22464679914735E-16,1.));
#45922=DIRECTION('center_axis',(-1.,0.,0.));
#45923=DIRECTION('ref_axis',(0.,-1.22464679914735E-16,-1.));
#45924=DIRECTION('center_axis',(0.,0.5,-0.866025403784439));
#45925=DIRECTION('ref_axis',(0.,-0.866025403784439,-0.5));
#45926=DIRECTION('center_axis',(0.,-1.,-2.10735636863952E-16));
#45927=DIRECTION('ref_axis',(0.,2.10735636863952E-16,-1.));
#45928=DIRECTION('center_axis',(1.,0.,0.));
#45929=DIRECTION('ref_axis',(0.,0.,-1.));
#61978=CARTESIAN_POINT('',(0.,0.,0.));
#61979=CARTESIAN_POINT('Origin',(15.65,-6.08813972081441,0.455032679971239));
#61980=CARTESIAN_POINT('',(15.4,-17.6561953920765,7.4225278703698));
#61981=CARTESIAN_POINT('',(15.9,-16.7109201357914,6.29942267750568));
#61982=CARTESIAN_POINT('Ctrl Pts',(15.4,-17.6561953920765,7.4225278703698));
#61983=CARTESIAN_POINT('Ctrl Pts',(15.659421374204,-17.1714233605295,6.84309060700005));
#61984=CARTESIAN_POINT('Ctrl Pts',(15.9,-16.7109201357914,6.29942267750568));
#61985=CARTESIAN_POINT('',(15.9,-12.6466233749287,3.95289984855508));
#61986=CARTESIAN_POINT('',(15.9,-6.21313972081441,0.238526329025129));
#61987=CARTESIAN_POINT('',(15.6433901317022,-12.3389772513248,4.071587819396));
#61988=CARTESIAN_POINT('Ctrl Pts',(15.9000000000344,-12.6466233749697,3.95289984853906));
#61989=CARTESIAN_POINT('Ctrl Pts',(15.7706592115056,-12.4922823846733,4.01314090443486));
#61990=CARTESIAN_POINT('Ctrl Pts',(15.6433901317022,-12.3389772513248,4.071587819396));
#61991=CARTESIAN_POINT('',(15.4,-12.4774525214495,4.43257927994945));
#61992=CARTESIAN_POINT('',(14.6907281821669,-12.8809881912407,5.48455725744013));
#61993=CARTESIAN_POINT('',(15.4,-5.96313972081441,0.671539030917348));
#61994=CARTESIAN_POINT('Origin',(15.9,0.,0.));
#61995=CARTESIAN_POINT('',(15.9,-16.7109201357914,-6.29942267750567));
#61996=CARTESIAN_POINT('Origin',(15.9,0.,0.));
#61997=CARTESIAN_POINT('',(15.9,-12.6466233749287,-3.95289984855507));
#61998=CARTESIAN_POINT('',(15.9,-11.409292143521,-3.23852632902513));
#61999=CARTESIAN_POINT('Origin',(15.9,0.,0.));
#62000=CARTESIAN_POINT('Origin',(15.15,0.,0.));
#62001=CARTESIAN_POINT('',(15.3288252219091,-17.8169872981078,7.51536112060047));
#62002=CARTESIAN_POINT('Ctrl Pts',(15.4,-17.6561953920765,7.4225278703698));
#62003=CARTESIAN_POINT('Ctrl Pts',(15.3645856261785,-17.736206562841,7.46872234134886));
#62004=CARTESIAN_POINT('Ctrl Pts',(15.3288252219091,-17.8169872981078,7.51536112060047));
#62005=CARTESIAN_POINT('',(15.2106539453059,-18.25,7.26536112060047));
#62006=CARTESIAN_POINT('Ctrl Pts',(15.2106539453059,-18.25,7.26536112060047));
#62007=CARTESIAN_POINT('Ctrl Pts',(15.2709785585168,-18.031794847786,7.39134192396977));
#62008=CARTESIAN_POINT('Ctrl Pts',(15.3288252219091,-17.8169872981078,7.51536112060047));
#62009=CARTESIAN_POINT('',(15.2106539453093,-18.25,-7.26536112060046));
#62010=CARTESIAN_POINT('Ctrl Pts',(15.2106539453093,-18.25,-7.26536112060046));
#62011=CARTESIAN_POINT('Ctrl Pts',(16.2489053918282,-18.25,-2.42950104478723E-11));
#62012=CARTESIAN_POINT('Ctrl Pts',(15.2106539453059,-18.25,7.26536112060047));
#62013=CARTESIAN_POINT('',(15.3288252219121,-17.8169872981078,-7.51536112060046));
#62014=CARTESIAN_POINT('Ctrl Pts',(15.3288252219121,-17.8169872981078,-7.51536112060046));
#62015=CARTESIAN_POINT('Ctrl Pts',(15.2709785585222,-18.0317948477897,-7.39134192396767));
#62016=CARTESIAN_POINT('Ctrl Pts',(15.2106539453093,-18.25,-7.26536112060046));
#62017=CARTESIAN_POINT('',(15.4,-17.656195392083,-7.42252787037352));
#62018=CARTESIAN_POINT('Ctrl Pts',(15.3288252219121,-17.8169872981078,-7.51536112060046));
#62019=CARTESIAN_POINT('Ctrl Pts',(15.3645856261806,-17.7362065628429,-7.46872234134997));
#62020=CARTESIAN_POINT('Ctrl Pts',(15.4,-17.656195392083,-7.42252787037352));
#62021=CARTESIAN_POINT('Ctrl Pts',(15.9,-16.7109201357914,-6.29942267750567));
#62022=CARTESIAN_POINT('Ctrl Pts',(15.6594213742066,-17.1714233605351,-6.84309060700024));
#62023=CARTESIAN_POINT('Ctrl Pts',(15.4,-17.656195392083,-7.42252787037352));
#62024=CARTESIAN_POINT('Origin',(15.9,-10.7262794416288,3.42153903091735));
#62025=CARTESIAN_POINT('',(9.89139647084341,-12.4774525214495,4.43257927994945));
#62026=CARTESIAN_POINT('',(0.,-12.4774525214495,4.43257927994945));
#62027=CARTESIAN_POINT('',(9.9,-12.4850287992543,4.43695344597952));
#62028=CARTESIAN_POINT('Ctrl Pts',(9.89999999999984,-12.4850287992542,4.43695344597944));
#62029=CARTESIAN_POINT('Ctrl Pts',(9.89569679092782,-12.4812394300896,4.43476565267222));
#62030=CARTESIAN_POINT('Ctrl Pts',(9.89139647084332,-12.4774525214494,4.43257927994941));
#62031=CARTESIAN_POINT('',(9.9,-17.75,7.47668598600566));
#62032=CARTESIAN_POINT('',(9.9,-21.1185842870421,9.42153903091735));
#62033=CARTESIAN_POINT('',(9.83301270189222,-17.8169872981078,7.51536112060047));
#62034=CARTESIAN_POINT('',(12.8327618786655,-14.8172381213345,5.78345512588906));
#62035=CARTESIAN_POINT('',(7.95,-17.8169872981078,7.51536112060047));
#62036=CARTESIAN_POINT('Origin',(7.95,-18.0334936490539,7.39036112060047));
#62037=CARTESIAN_POINT('',(9.4,-18.25,7.26536112060047));
#62038=CARTESIAN_POINT('',(9.53701905283833,-18.1129809471617,7.34446910764079));
#62039=CARTESIAN_POINT('',(7.95,-18.25,7.26536112060047));
#62040=CARTESIAN_POINT('Origin',(7.95,-18.0334936490539,-7.39036112060046));
#62041=CARTESIAN_POINT('',(9.83301270189222,-17.8169872981078,-7.51536112060046));
#62042=CARTESIAN_POINT('',(7.95,-17.8169872981078,-7.51536112060046));
#62043=CARTESIAN_POINT('',(9.4,-18.25,-7.26536112060046));
#62044=CARTESIAN_POINT('',(7.95,-18.25,-7.26536112060046));
#62045=CARTESIAN_POINT('',(9.4,-18.25,-7.26536112060046));
#62046=CARTESIAN_POINT('Origin',(9.65,-18.,1.01832120635534));
#62047=CARTESIAN_POINT('',(9.4,-18.25,-10.0366424127107));
#62048=CARTESIAN_POINT('',(9.4,-18.25,1.01832120635534));
#62049=CARTESIAN_POINT('',(9.61650635094611,-18.0334936490539,-10.4116424127107));
#62050=CARTESIAN_POINT('',(6.68182667397366,-20.9681733260263,-5.32862810825457));
#62051=CARTESIAN_POINT('',(9.9,-17.75,-10.2479672781159));
#62052=CARTESIAN_POINT('',(11.1698262954046,-16.4801737045954,-9.51483272463993));
#62053=CARTESIAN_POINT('',(9.9,-17.75,-7.47668598600565));
#62054=CARTESIAN_POINT('',(9.9,-17.75,1.01832120635534));
#62055=CARTESIAN_POINT('',(11.1671033514046,-16.4828966485954,-6.74512352498115));
#62056=CARTESIAN_POINT('Origin',(15.9,-21.1185842870421,-9.42153903091734));
#62057=CARTESIAN_POINT('',(9.9,-12.4850287992543,-4.43695344597952));
#62058=CARTESIAN_POINT('',(9.9,-10.7262794416288,-3.42153903091735));
#62059=CARTESIAN_POINT('',(9.8913964708434,-12.4774525214495,-4.43257927994945));
#62060=CARTESIAN_POINT('Ctrl Pts',(9.89139647084313,-12.4774525214493,-4.43257927994931));
#62061=CARTESIAN_POINT('Ctrl Pts',(9.89569679092766,-12.4812394300895,-4.43476565267213));
#62062=CARTESIAN_POINT('Ctrl Pts',(9.89999999999972,-12.4850287992541,-4.43695344597938));
#62063=CARTESIAN_POINT('',(15.4,-12.4774525214495,-4.43257927994945));
#62064=CARTESIAN_POINT('',(0.,-12.4774525214495,-4.43257927994945));
#62065=CARTESIAN_POINT('',(15.4,-11.159292143521,-3.67153903091734));
#62066=CARTESIAN_POINT('Origin',(9.9,-14.7224318643355,-8.5));
#62067=CARTESIAN_POINT('',(9.9,-15.35,-11.633607924171));
#62068=CARTESIAN_POINT('',(9.9,-17.1181079660839,-10.6127903139961));
#62069=CARTESIAN_POINT('',(9.9,-10.0850287992543,-8.59387538414482));
#62070=CARTESIAN_POINT('',(9.9,-18.7185842870421,-13.5784609690826));
#62071=CARTESIAN_POINT('Origin',(9.9,0.,0.));
#62072=CARTESIAN_POINT('Origin',(9.65,-17.2431079660839,-10.8292966649422));
#62073=CARTESIAN_POINT('',(9.4,-17.8169872981078,-10.7866424127107));
#62074=CARTESIAN_POINT('',(9.83301270189222,-18.25,-10.0366424127107));
#62075=CARTESIAN_POINT('',(9.4,-15.4169872981078,-12.1722830587658));
#62076=CARTESIAN_POINT('',(9.4,-17.3681079660839,-11.0458030158883));
#62077=CARTESIAN_POINT('',(9.83301270189222,-15.4169872981078,-11.6722830587658));
#62078=CARTESIAN_POINT('',(9.83301270189222,-15.4169872981078,-11.6722830587658));
#62079=CARTESIAN_POINT('',(12.8327618786655,-12.4172381213345,-9.94037706405436));
#62080=CARTESIAN_POINT('Origin',(15.65,-11.284292143521,-3.45503267997124));
#62081=CARTESIAN_POINT('',(15.6433901317022,-12.3389772513248,-4.07158781939599));
#62082=CARTESIAN_POINT('Ctrl Pts',(15.6433901317022,-12.3389772513248,-4.07158781939599));
#62083=CARTESIAN_POINT('Ctrl Pts',(15.7706592115054,-12.4922823846731,-4.01314090443493));
#62084=CARTESIAN_POINT('Ctrl Pts',(15.9000000000344,-12.6466233749697,-3.95289984853905));
#62085=CARTESIAN_POINT('',(13.6398107279463,-13.4789009633564,-7.04325730755368));
#62086=CARTESIAN_POINT('Origin',(15.65,0.,0.));
#62087=CARTESIAN_POINT('',(15.4,-12.1991696110502,-3.70712298161641));
#62088=CARTESIAN_POINT('Ctrl Pts',(15.6433901273902,-12.3389772534808,-4.0715878156617));
#62089=CARTESIAN_POINT('Ctrl Pts',(15.5613792592266,-12.2925524049577,-3.95056278141904));
#62090=CARTESIAN_POINT('Ctrl Pts',(15.4801979882799,-12.2459386469402,-3.82904527862226));
#62091=CARTESIAN_POINT('Ctrl Pts',(15.4,-12.1991696110502,-3.70712298161641));
#62092=CARTESIAN_POINT('',(15.4,-12.1991696110502,3.70712298161641));
#62093=CARTESIAN_POINT('Origin',(15.4,0.,0.));
#62094=CARTESIAN_POINT('Ctrl Pts',(15.6433901273902,-12.3389772534808,4.0715878156617));
#62095=CARTESIAN_POINT('Ctrl Pts',(15.5613792592266,-12.2925524049577,3.95056278141906));
#62096=CARTESIAN_POINT('Ctrl Pts',(15.4801979882799,-12.2459386469402,3.82904527862227));
#62097=CARTESIAN_POINT('Ctrl Pts',(15.4,-12.1991696110502,3.70712298161641));
#62098=CARTESIAN_POINT('Origin',(0.,-18.0334936490539,10.4116424127107));
#62099=CARTESIAN_POINT('',(9.61650635094611,-18.0334936490539,10.4116424127107));
#62100=CARTESIAN_POINT('',(9.4,-17.8169872981078,10.7866424127107));
#62101=CARTESIAN_POINT('',(6.68182667397368,-15.0988139720814,15.4946567171668));
#62102=CARTESIAN_POINT('',(1.14709933354294,-17.8169872981078,10.7866424127107));
#62103=CARTESIAN_POINT('',(0.,-17.8169872981078,10.7866424127107));
#62104=CARTESIAN_POINT('',(1.14709933354217,-18.25,10.0366424127107));
#62105=CARTESIAN_POINT('Ctrl Pts',(1.14709933354294,-17.8169872981078,10.7866424127107));
#62106=CARTESIAN_POINT('Ctrl Pts',(1.14362113475313,-18.0334936490539,10.4116424127107));
#62107=CARTESIAN_POINT('Ctrl Pts',(1.14709933354217,-18.25,10.0366424127107));
#62108=CARTESIAN_POINT('',(9.4,-18.25,10.0366424127107));
#62109=CARTESIAN_POINT('',(0.,-18.25,10.0366424127107));
#62110=CARTESIAN_POINT('',(8.50682667397365,-19.1431733260264,8.48962083206777));
#62111=CARTESIAN_POINT('Origin',(0.,1.29036654044864E-15,21.0732848254213));
#62112=CARTESIAN_POINT('',(9.4,-15.4169872981078,12.1722830587658));
#62113=CARTESIAN_POINT('',(9.4,-8.24310796608386,16.3141242222437));
#62114=CARTESIAN_POINT('',(15.2106539453093,-15.4169872981078,12.1722830587658));
#62115=CARTESIAN_POINT('',(7.95,-15.4169872981078,12.1722830587658));
#62116=CARTESIAN_POINT('',(15.2106539453059,-2.83301270189222,19.4376441793662));
#62117=CARTESIAN_POINT('Ctrl Pts',(15.2106539453093,-15.4169872981078,12.1722830587658));
#62118=CARTESIAN_POINT('Ctrl Pts',(16.2489053918282,-9.12500000002104,15.8049636190539));
#62119=CARTESIAN_POINT('Ctrl Pts',(15.2106539453059,-2.83301270189222,19.4376441793663));
#62120=CARTESIAN_POINT('',(9.4,-2.83301270189222,19.4376441793662));
#62121=CARTESIAN_POINT('',(3.975,-2.83301270189222,19.4376441793662));
#62122=CARTESIAN_POINT('',(9.4,-0.433012701892218,20.8232848254213));
#62123=CARTESIAN_POINT('',(9.4,-0.881892033916136,20.5641242222437));
#62124=CARTESIAN_POINT('',(1.14709933354217,-0.433012701892219,20.8232848254213));
#62125=CARTESIAN_POINT('',(0.,-0.433012701892218,20.8232848254213));
#62126=CARTESIAN_POINT('Ctrl Pts',(1.14709933354217,-0.433012701892218,
20.8232848254213));
#62127=CARTESIAN_POINT('Ctrl Pts',(-0.721559551129004,-9.12499999996429,
15.8049636190866));
#62128=CARTESIAN_POINT('Ctrl Pts',(1.14709933354294,-17.8169872981078,10.7866424127107));
#62129=CARTESIAN_POINT('Origin',(9.65,-8.11810796608386,16.0976178712976));
#62130=CARTESIAN_POINT('',(9.9,-17.75,10.2479672781159));
#62131=CARTESIAN_POINT('',(9.9,-17.75,10.2479672781159));
#62132=CARTESIAN_POINT('',(9.9,-15.35,11.633607924171));
#62133=CARTESIAN_POINT('',(9.9,-7.99310796608386,15.8811115203515));
#62134=CARTESIAN_POINT('',(9.83301270189222,-15.4169872981078,11.6722830587658));
#62135=CARTESIAN_POINT('',(11.1671033514046,-14.0828966485954,10.9020454631465));
#62136=CARTESIAN_POINT('',(9.4,-15.4169872981078,12.1722830587658));
#62137=CARTESIAN_POINT('Origin',(9.65,-18.,9.51832120635533));
#62138=CARTESIAN_POINT('',(9.4,-18.25,9.51832120635533));
#62139=CARTESIAN_POINT('',(9.9,-17.75,9.51832120635533));
#62140=CARTESIAN_POINT('Origin',(15.65,-3.43813972081441,-5.04496732002876));
#62141=CARTESIAN_POINT('',(15.4,-15.2561953920766,-11.5794498085352));
#62142=CARTESIAN_POINT('',(15.9,-13.8109201357914,-11.3223700194554));
#62143=CARTESIAN_POINT('Ctrl Pts',(15.4,-15.2561953920766,-11.5794498085352));
#62144=CARTESIAN_POINT('Ctrl Pts',(15.659421374204,-14.5120019863256,-11.4493435458561));
#62145=CARTESIAN_POINT('Ctrl Pts',(15.9,-13.8109201357914,-11.3223700194554));
#62146=CARTESIAN_POINT('',(15.9,-9.74662337492871,-8.97584719050482));
#62147=CARTESIAN_POINT('',(15.9,-3.31313972081441,-5.26147367097487));
#62148=CARTESIAN_POINT('',(15.6433901317022,-9.6955871109986,-8.65007384666752));
#62149=CARTESIAN_POINT('Ctrl Pts',(15.9000000000343,-9.74662337493534,-8.97584719054823));
#62150=CARTESIAN_POINT('Ctrl Pts',(15.7706592115056,-9.72162316454368,-8.81206344415842));
#62151=CARTESIAN_POINT('Ctrl Pts',(15.6433901317022,-9.6955871109986,-8.65007384666752));
#62152=CARTESIAN_POINT('',(15.4,-10.0774525214495,-8.58950121811475));
#62153=CARTESIAN_POINT('',(14.6907281821669,-11.1902600090738,-8.41298437074177));
#62154=CARTESIAN_POINT('',(15.4,-3.56313972081441,-4.82846096908265));
#62155=CARTESIAN_POINT('Origin',(15.65,0.,0.));
#62156=CARTESIAN_POINT('',(15.9,-2.9,-12.9287470390599));
#62157=CARTESIAN_POINT('Origin',(15.9,0.,0.));
#62158=CARTESIAN_POINT('',(15.6433901317022,-2.64339014032616,-12.7216616660635));
#62159=CARTESIAN_POINT('Ctrl Pts',(15.6433901317022,-2.64339014032616,-12.7216616660635));
#62160=CARTESIAN_POINT('Ctrl Pts',(15.7706592115055,-2.77065922012951,-12.8252043485933));
#62161=CARTESIAN_POINT('Ctrl Pts',(15.9000000000343,-2.90000000003428,-12.9287470390873));
#62162=CARTESIAN_POINT('',(15.4,-2.88912212849219,-12.4183522790528));
#62163=CARTESIAN_POINT('Ctrl Pts',(15.6433901273902,-2.64339014463815,-12.7216616660635));
#62164=CARTESIAN_POINT('Ctrl Pts',(15.5613792592266,-2.72498847452463,-12.6209440507544));
#62165=CARTESIAN_POINT('Ctrl Pts',(15.4801979882799,-2.80691883994237,-12.519816600747));
#62166=CARTESIAN_POINT('Ctrl Pts',(15.4,-2.88912212849219,-12.4183522790528));
#62167=CARTESIAN_POINT('',(15.4,-9.31004748255804,-8.71122929743642));
#62168=CARTESIAN_POINT('Origin',(15.4,0.,0.));
#62169=CARTESIAN_POINT('Ctrl Pts',(15.4,-9.31004748255804,-8.71122929743642));
#62170=CARTESIAN_POINT('Ctrl Pts',(15.4801979882799,-9.43901980699785,-8.69077132212473));
#62171=CARTESIAN_POINT('Ctrl Pts',(15.5613792592266,-9.56756393043304,-8.67038126933532));
#62172=CARTESIAN_POINT('Ctrl Pts',(15.6433901273902,-9.6955871088426,-8.65007385040182));
#62173=CARTESIAN_POINT('Origin',(15.9,0.,0.));
#62174=CARTESIAN_POINT('',(15.9,-2.9,-17.6217926969611));
#62175=CARTESIAN_POINT('Origin',(15.9,0.,0.));
#62176=CARTESIAN_POINT('',(15.9,-2.9,-11.5));
#62177=CARTESIAN_POINT('Origin',(15.15,0.,0.));
#62178=CARTESIAN_POINT('',(15.3288252219092,-15.4169872981078,-11.6722830587658));
#62179=CARTESIAN_POINT('Ctrl Pts',(15.4,-15.2561953920766,-11.5794498085352));
#62180=CARTESIAN_POINT('Ctrl Pts',(15.3645856261792,-15.3362065628395,-11.6256442795133));
#62181=CARTESIAN_POINT('Ctrl Pts',(15.3288252219092,-15.4169872981078,-11.6722830587658));
#62182=CARTESIAN_POINT('',(15.2106539453059,-15.4169872981078,-12.1722830587658));
#62183=CARTESIAN_POINT('Ctrl Pts',(15.2106539453059,-15.4169872981078,-12.1722830587658));
#62184=CARTESIAN_POINT('Ctrl Pts',(15.2709785585169,-15.4169872981078,-11.9203214520272));
#62185=CARTESIAN_POINT('Ctrl Pts',(15.3288252219092,-15.4169872981078,-11.6722830587658));
#62186=CARTESIAN_POINT('',(15.2106539453093,-2.83301270189222,-19.4376441793662));
#62187=CARTESIAN_POINT('Ctrl Pts',(15.2106539453093,-2.83301270189223,-19.4376441793662));
#62188=CARTESIAN_POINT('Ctrl Pts',(16.2489053918282,-9.12499999997897,-15.8049636190782));
#62189=CARTESIAN_POINT('Ctrl Pts',(15.2106539453059,-15.4169872981078,-12.1722830587658));
#62190=CARTESIAN_POINT('',(15.3288252219121,-2.4,-19.1876441793662));
#62191=CARTESIAN_POINT('Ctrl Pts',(15.3288252219121,-2.4,-19.1876441793662));
#62192=CARTESIAN_POINT('Ctrl Pts',(15.2709785585222,-2.61480754968187,-19.311663375999));
#62193=CARTESIAN_POINT('Ctrl Pts',(15.2106539453093,-2.83301270189222,-19.4376441793662));
#62194=CARTESIAN_POINT('',(15.4,-2.4,-19.0019776789123));
#62195=CARTESIAN_POINT('Ctrl Pts',(15.3288252219121,-2.4,-19.1876441793662));
#62196=CARTESIAN_POINT('Ctrl Pts',(15.3645856261801,-2.4,-19.0943666208664));
#62197=CARTESIAN_POINT('Ctrl Pts',(15.4,-2.4,-19.0019776789123));
#62198=CARTESIAN_POINT('Ctrl Pts',(15.9,-2.9,-17.6217926969611));
#62199=CARTESIAN_POINT('Ctrl Pts',(15.6594213742066,-2.65942137420663,-18.292434152861));
#62200=CARTESIAN_POINT('Ctrl Pts',(15.4,-2.4,-19.0019776789123));
#62201=CARTESIAN_POINT('Origin',(7.95,-15.4169872981078,-11.9222830587658));
#62202=CARTESIAN_POINT('',(7.95,-15.4169872981078,-12.1722830587658));
#62203=CARTESIAN_POINT('',(7.95,-15.4169872981078,-11.6722830587658));
#62204=CARTESIAN_POINT('Origin',(0.,-18.0334936490539,-10.4116424127107));
#62205=CARTESIAN_POINT('',(1.14709933354294,-18.25,-10.0366424127107));
#62206=CARTESIAN_POINT('',(0.,-18.25,-10.0366424127107));
#62207=CARTESIAN_POINT('',(1.14709933354217,-17.8169872981078,-10.7866424127107));
#62208=CARTESIAN_POINT('Ctrl Pts',(1.14709933354294,-18.25,-10.0366424127107));
#62209=CARTESIAN_POINT('Ctrl Pts',(1.14362113475313,-18.0334936490539,-10.4116424127107));
#62210=CARTESIAN_POINT('Ctrl Pts',(1.14709933354217,-17.8169872981078,-10.7866424127107));
#62211=CARTESIAN_POINT('',(0.,-17.8169872981078,-10.7866424127107));
#62212=CARTESIAN_POINT('Origin',(0.,-18.25,-10.5366424127107));
#62213=CARTESIAN_POINT('',(1.14709933354294,-0.433012701892223,-20.8232848254213));
#62214=CARTESIAN_POINT('Ctrl Pts',(1.14709933354217,-17.8169872981078,-10.7866424127107));
#62215=CARTESIAN_POINT('Ctrl Pts',(-0.721559551129003,-9.12500000003573,
-15.8049636190454));
#62216=CARTESIAN_POINT('Ctrl Pts',(1.14709933354294,-0.433012701892223,
-20.8232848254213));
#62217=CARTESIAN_POINT('',(9.4,-0.433012701892223,-20.8232848254213));
#62218=CARTESIAN_POINT('',(0.,-0.433012701892223,-20.8232848254213));
#62219=CARTESIAN_POINT('',(9.4,-2.83301270189222,-19.4376441793662));
#62220=CARTESIAN_POINT('',(9.4,-10.0068920339161,-15.2958030158883));
#62221=CARTESIAN_POINT('',(7.95,-2.83301270189222,-19.4376441793662));
#62222=CARTESIAN_POINT('Origin',(0.75,0.,0.));
#62223=CARTESIAN_POINT('',(0.,-17.8588235294118,2.18707510718316E-15));
#62224=CARTESIAN_POINT('Origin',(0.,0.,0.));
#62225=CARTESIAN_POINT('',(0.151136363625822,-18.25,-5.64802764011468E-15));
#62226=CARTESIAN_POINT('',(0.75,-19.8,-2.42480066231176E-15));
#62227=CARTESIAN_POINT('Ctrl Pts',(1.14709933354217,-18.25,10.0366424127107));
#62228=CARTESIAN_POINT('Ctrl Pts',(0.15113636362346,-18.25,4.68728503810705));
#62229=CARTESIAN_POINT('Ctrl Pts',(0.151136363625822,-18.25,-9.06107487178543E-15));
#62230=CARTESIAN_POINT('',(1.14709933354294,0.433012701892216,20.8232848254213));
#62231=CARTESIAN_POINT('Ctrl Pts',(1.14709933354294,0.433012701892216,20.8232848254213));
#62232=CARTESIAN_POINT('Ctrl Pts',(1.14362113475313,-8.04911692853238E-15,
20.8232848254213));
#62233=CARTESIAN_POINT('Ctrl Pts',(1.14709933354217,-0.433012701892219,
20.8232848254213));
#62234=CARTESIAN_POINT('',(1.14709933354217,17.8169872981078,10.7866424127107));
#62235=CARTESIAN_POINT('Ctrl Pts',(1.14709933354217,17.8169872981078,10.7866424127107));
#62236=CARTESIAN_POINT('Ctrl Pts',(-0.721559551129003,9.12500000003573,
15.8049636190454));
#62237=CARTESIAN_POINT('Ctrl Pts',(1.14709933354294,0.433012701892217,20.8232848254213));
#62238=CARTESIAN_POINT('',(1.14709933354294,18.25,10.0366424127107));
#62239=CARTESIAN_POINT('Ctrl Pts',(1.14709933354294,18.25,10.0366424127107));
#62240=CARTESIAN_POINT('Ctrl Pts',(1.14362113475313,18.0334936490539,10.4116424127107));
#62241=CARTESIAN_POINT('Ctrl Pts',(1.14709933354217,17.8169872981078,10.7866424127107));
#62242=CARTESIAN_POINT('',(1.14709933354217,18.25,-10.0366424127107));
#62243=CARTESIAN_POINT('Ctrl Pts',(1.14709933354217,18.25,-10.0366424127107));
#62244=CARTESIAN_POINT('Ctrl Pts',(-0.721559551129004,18.25,-4.12425649187753E-11));
#62245=CARTESIAN_POINT('Ctrl Pts',(1.14709933354294,18.25,10.0366424127107));
#62246=CARTESIAN_POINT('',(1.14709933354294,17.8169872981078,-10.7866424127107));
#62247=CARTESIAN_POINT('Ctrl Pts',(1.14709933354294,17.8169872981078,-10.7866424127107));
#62248=CARTESIAN_POINT('Ctrl Pts',(1.14362113475313,18.0334936490539,-10.4116424127107));
#62249=CARTESIAN_POINT('Ctrl Pts',(1.14709933354217,18.25,-10.0366424127107));
#62250=CARTESIAN_POINT('',(1.14709933354217,0.433012701892212,-20.8232848254213));
#62251=CARTESIAN_POINT('Ctrl Pts',(1.14709933354217,0.433012701892213,-20.8232848254213));
#62252=CARTESIAN_POINT('Ctrl Pts',(-0.721559551129003,9.12499999996428,
-15.8049636190866));
#62253=CARTESIAN_POINT('Ctrl Pts',(1.14709933354294,17.8169872981078,-10.7866424127107));
#62254=CARTESIAN_POINT('Ctrl Pts',(1.14709933354294,-0.433012701892223,
-20.8232848254213));
#62255=CARTESIAN_POINT('Ctrl Pts',(1.14362113475313,1.66533453693773E-15,
-20.8232848254213));
#62256=CARTESIAN_POINT('Ctrl Pts',(1.14709933354217,0.433012701892212,-20.8232848254213));
#62257=CARTESIAN_POINT('Ctrl Pts',(0.151136363625822,-18.25,-9.06107487178543E-15));
#62258=CARTESIAN_POINT('Ctrl Pts',(0.151136363628184,-18.25,-4.68728503808653));
#62259=CARTESIAN_POINT('Ctrl Pts',(1.14709933354294,-18.25,-10.0366424127107));
#62260=CARTESIAN_POINT('Origin',(15.65,2.65,-5.5));
#62261=CARTESIAN_POINT('',(15.4,2.4,-19.0019776789049));
#62262=CARTESIAN_POINT('',(15.9,2.9,-17.6217926969611));
#62263=CARTESIAN_POINT('Ctrl Pts',(15.4,2.4,-19.0019776789049));
#62264=CARTESIAN_POINT('Ctrl Pts',(15.6594213742041,2.65942137420405,-18.2924341528561));
#62265=CARTESIAN_POINT('Ctrl Pts',(15.9,2.9,-17.6217926969611));
#62266=CARTESIAN_POINT('',(15.9,2.9,-12.9287470390599));
#62267=CARTESIAN_POINT('',(15.9,2.9,-5.5));
#62268=CARTESIAN_POINT('',(15.6433901317022,2.64339014032616,-12.7216616660635));
#62269=CARTESIAN_POINT('Ctrl Pts',(15.9000000000343,2.90000000003429,-12.9287470390873));
#62270=CARTESIAN_POINT('Ctrl Pts',(15.7706592115055,2.77065922012948,-12.8252043485932));
#62271=CARTESIAN_POINT('Ctrl Pts',(15.6433901317022,2.64339014032616,-12.7216616660635));
#62272=CARTESIAN_POINT('',(15.4,2.4,-13.0220804980642));
#62273=CARTESIAN_POINT('',(14.6907281821669,1.6907281821669,-13.8975416281819));
#62274=CARTESIAN_POINT('',(15.4,2.4,-5.5));
#62275=CARTESIAN_POINT('Origin',(15.9,0.,0.));
#62276=CARTESIAN_POINT('',(15.9,13.8109201357914,-11.3223700194554));
#62277=CARTESIAN_POINT('Origin',(15.9,0.,0.));
#62278=CARTESIAN_POINT('',(15.9,9.74662337492871,-8.97584719050482));
#62279=CARTESIAN_POINT('',(15.9,8.50929214352104,-8.26147367097488));
#62280=CARTESIAN_POINT('Origin',(15.9,0.,0.));
#62281=CARTESIAN_POINT('Origin',(15.15,0.,0.));
#62282=CARTESIAN_POINT('',(15.3288252219091,2.4,-19.1876441793662));
#62283=CARTESIAN_POINT('Ctrl Pts',(15.4,2.4,-19.0019776789049));
#62284=CARTESIAN_POINT('Ctrl Pts',(15.3645856261785,2.4,-19.094366620863));
#62285=CARTESIAN_POINT('Ctrl Pts',(15.3288252219091,2.4,-19.1876441793662));
#62286=CARTESIAN_POINT('',(15.2106539453059,2.83301270189221,-19.4376441793662));
#62287=CARTESIAN_POINT('Ctrl Pts',(15.2106539453059,2.83301270189221,-19.4376441793662));
#62288=CARTESIAN_POINT('Ctrl Pts',(15.2709785585168,2.61480754967825,-19.3116633759969));
#62289=CARTESIAN_POINT('Ctrl Pts',(15.3288252219091,2.4,-19.1876441793662));
#62290=CARTESIAN_POINT('',(15.2106539453093,15.4169872981078,-12.1722830587658));
#62291=CARTESIAN_POINT('Ctrl Pts',(15.2106539453093,15.4169872981078,-12.1722830587658));
#62292=CARTESIAN_POINT('Ctrl Pts',(16.2489053918282,9.12500000002104,-15.8049636190539));
#62293=CARTESIAN_POINT('Ctrl Pts',(15.2106539453059,2.83301270189221,-19.4376441793662));
#62294=CARTESIAN_POINT('',(15.3288252219121,15.4169872981078,-11.6722830587658));
#62295=CARTESIAN_POINT('Ctrl Pts',(15.3288252219121,15.4169872981078,-11.6722830587658));
#62296=CARTESIAN_POINT('Ctrl Pts',(15.2709785585222,15.4169872981078,-11.9203214520314));
#62297=CARTESIAN_POINT('Ctrl Pts',(15.2106539453093,15.4169872981078,-12.1722830587658));
#62298=CARTESIAN_POINT('',(15.4,15.256195392083,-11.5794498085389));
#62299=CARTESIAN_POINT('Ctrl Pts',(15.3288252219121,15.4169872981078,-11.6722830587658));
#62300=CARTESIAN_POINT('Ctrl Pts',(15.3645856261809,15.3362065628422,-11.6256442795149));
#62301=CARTESIAN_POINT('Ctrl Pts',(15.4,15.256195392083,-11.5794498085389));
#62302=CARTESIAN_POINT('Ctrl Pts',(15.9,13.8109201357914,-11.3223700194554));
#62303=CARTESIAN_POINT('Ctrl Pts',(15.6594213742065,14.5120019863289,-11.4493435458609));
#62304=CARTESIAN_POINT('Ctrl Pts',(15.4,15.256195392083,-11.5794498085389));
#62305=CARTESIAN_POINT('Origin',(15.9,2.4,-11.));
#62306=CARTESIAN_POINT('',(9.89139647084341,2.4,-13.0220804980642));
#62307=CARTESIAN_POINT('',(0.,2.4,-13.0220804980642));
#62308=CARTESIAN_POINT('',(9.9,2.4,-13.0308288301244));
#62309=CARTESIAN_POINT('Ctrl Pts',(9.89999999999984,2.4,-13.0308288301242));
#62310=CARTESIAN_POINT('Ctrl Pts',(9.89569679092782,2.4,-13.0264532435097));
#62311=CARTESIAN_POINT('Ctrl Pts',(9.89139647084332,2.4,-13.0220804980641));
#62312=CARTESIAN_POINT('',(9.9,2.4,-19.1102939101766));
#62313=CARTESIAN_POINT('',(9.9,2.4,-23.));
#62314=CARTESIAN_POINT('',(9.83301270189222,2.4,-19.1876441793662));
#62315=CARTESIAN_POINT('',(12.8327618786655,2.4,-15.7238321899434));
#62316=CARTESIAN_POINT('',(7.95,2.4,-19.1876441793662));
#62317=CARTESIAN_POINT('Origin',(7.95,2.61650635094611,-19.3126441793662));
#62318=CARTESIAN_POINT('',(9.4,2.83301270189222,-19.4376441793662));
#62319=CARTESIAN_POINT('',(7.95,2.83301270189222,-19.4376441793662));
#62320=CARTESIAN_POINT('',(9.83301270189222,2.4,-19.1876441793662));
#62321=CARTESIAN_POINT('Origin',(9.9,-1.66533453693773E-15,-20.4959345562317));
#62322=CARTESIAN_POINT('',(9.4,0.433012701892213,-20.8232848254213));
#62323=CARTESIAN_POINT('',(9.4,0.433012701892213,-20.8232848254213));
#62324=CARTESIAN_POINT('',(9.9,2.22044604925031E-15,-20.4959345562317));
#62325=CARTESIAN_POINT('',(9.9,-1.66533453693773E-15,-20.4959345562317));
#62326=CARTESIAN_POINT('',(9.4,-0.43301270189222,-20.8232848254213));
#62327=CARTESIAN_POINT('Origin',(9.65,0.756892033916132,-20.3476178712976));
#62328=CARTESIAN_POINT('',(9.9,0.631892033916133,-20.1311115203515));
#62329=CARTESIAN_POINT('',(9.4,0.881892033916132,-20.5641242222437));
#62330=CARTESIAN_POINT('Origin',(7.95,-2.61650635094611,-19.3126441793662));
#62331=CARTESIAN_POINT('',(9.83301270189222,-2.4,-19.1876441793662));
#62332=CARTESIAN_POINT('',(7.95,-2.4,-19.1876441793662));
#62333=CARTESIAN_POINT('',(9.4,-2.83301270189222,-19.4376441793662));
#62334=CARTESIAN_POINT('Origin',(9.65,-9.88189203391614,-15.0792966649422));
#62335=CARTESIAN_POINT('',(9.9,-2.4,-19.1102939101766));
#62336=CARTESIAN_POINT('',(9.9,-9.75689203391614,-14.8627903139961));
#62337=CARTESIAN_POINT('',(11.1671033514046,-2.4,-17.6471689881276));
#62338=CARTESIAN_POINT('Origin',(0.,-5.30825383648903E-15,-20.8232848254213));
#62339=CARTESIAN_POINT('',(0.,0.433012701892213,-20.8232848254213));
#62340=CARTESIAN_POINT('Origin',(0.,-3.87109962134591E-15,-21.0732848254213));
#62341=CARTESIAN_POINT('',(9.4,17.8169872981078,-10.7866424127107));
#62342=CARTESIAN_POINT('',(0.,17.8169872981078,-10.7866424127107));
#62343=CARTESIAN_POINT('',(9.4,15.4169872981078,-12.1722830587658));
#62344=CARTESIAN_POINT('',(9.4,8.24310796608386,-16.3141242222437));
#62345=CARTESIAN_POINT('',(7.95,15.4169872981078,-12.1722830587658));
#62346=CARTESIAN_POINT('Origin',(15.65,-2.65,-11.5));
#62347=CARTESIAN_POINT('',(15.4,-2.4,-13.0220804980642));
#62348=CARTESIAN_POINT('',(15.4,-2.4,-11.5));
#62349=CARTESIAN_POINT('',(13.6398107279464,-0.639810727946355,-15.1946993031381));
#62350=CARTESIAN_POINT('Origin',(7.95,15.4169872981078,-11.9222830587658));
#62351=CARTESIAN_POINT('',(9.83301270189222,15.4169872981078,-11.6722830587658));
#62352=CARTESIAN_POINT('',(7.95,15.4169872981078,-11.6722830587658));
#62353=CARTESIAN_POINT('',(9.4,15.4169872981078,-12.1722830587658));
#62354=CARTESIAN_POINT('Origin',(9.65,8.11810796608386,-16.0976178712976));
#62355=CARTESIAN_POINT('',(9.61650635094611,18.0334936490539,-10.4116424127107));
#62356=CARTESIAN_POINT('',(6.68182667397365,15.0988139720815,-15.4946567171668));
#62357=CARTESIAN_POINT('',(9.9,17.75,-10.2479672781159));
#62358=CARTESIAN_POINT('',(11.1698262954046,16.4801737045954,-9.51483272463995));
#62359=CARTESIAN_POINT('',(9.9,15.35,-11.633607924171));
#62360=CARTESIAN_POINT('',(9.9,7.99310796608386,-15.8811115203515));
#62361=CARTESIAN_POINT('',(11.1671033514046,14.0828966485954,-10.9020454631465));
#62362=CARTESIAN_POINT('Origin',(15.9,18.7185842870421,-13.5784609690827));
#62363=CARTESIAN_POINT('',(9.9,10.0850287992543,-8.59387538414483));
#62364=CARTESIAN_POINT('',(9.9,8.32627944162882,-7.57846096908266));
#62365=CARTESIAN_POINT('',(9.89139647084341,10.0774525214495,-8.58950121811476));
#62366=CARTESIAN_POINT('Ctrl Pts',(9.89139647084313,10.0774525214493,-8.58950121811462));
#62367=CARTESIAN_POINT('Ctrl Pts',(9.89569679092767,10.0812394300895,-8.59168759083745));
#62368=CARTESIAN_POINT('Ctrl Pts',(9.89999999999973,10.0850287992541,-8.59387538414469));
#62369=CARTESIAN_POINT('',(15.4,10.0774525214495,-8.58950121811476));
#62370=CARTESIAN_POINT('',(0.,10.0774525214495,-8.58950121811476));
#62371=CARTESIAN_POINT('',(15.4,8.75929214352104,-7.82846096908266));
#62372=CARTESIAN_POINT('Origin',(9.9,14.7224318643355,-8.50000000000001));
#62373=CARTESIAN_POINT('',(9.9,17.75,-7.47668598600567));
#62374=CARTESIAN_POINT('',(9.9,17.75,-9.51832120635534));
#62375=CARTESIAN_POINT('',(9.9,12.4850287992543,-4.43695344597953));
#62376=CARTESIAN_POINT('',(9.9,21.1185842870421,-9.42153903091736));
#62377=CARTESIAN_POINT('Origin',(9.9,0.,0.));
#62378=CARTESIAN_POINT('Origin',(9.65,18.,-9.51832120635534));
#62379=CARTESIAN_POINT('',(9.4,18.25,-10.0366424127107));
#62380=CARTESIAN_POINT('',(9.83301270189222,17.8169872981078,-10.7866424127107));
#62381=CARTESIAN_POINT('',(9.4,18.25,-7.26536112060048));
#62382=CARTESIAN_POINT('',(9.4,18.25,-9.51832120635534));
#62383=CARTESIAN_POINT('',(9.83301270189222,17.8169872981078,-7.51536112060048));
#62384=CARTESIAN_POINT('',(9.83301270189222,17.8169872981078,-7.51536112060048));
#62385=CARTESIAN_POINT('',(12.8327618786655,14.8172381213345,-5.78345512588907));
#62386=CARTESIAN_POINT('Origin',(15.65,8.63429214352104,-8.04496732002877));
#62387=CARTESIAN_POINT('',(15.6433901317022,9.69558711099859,-8.65007384666753));
#62388=CARTESIAN_POINT('Ctrl Pts',(15.6433901317022,9.69558711099859,-8.65007384666753));
#62389=CARTESIAN_POINT('Ctrl Pts',(15.7706592115056,9.72162316454367,-8.81206344415844));
#62390=CARTESIAN_POINT('Ctrl Pts',(15.9000000000343,9.74662337493534,-8.97584719054825));
#62391=CARTESIAN_POINT('',(13.6398107279463,12.8390902354101,-8.15144199558439));
#62392=CARTESIAN_POINT('Origin',(15.65,0.,0.));
#62393=CARTESIAN_POINT('',(15.4,9.31004748255804,-8.71122929743643));
#62394=CARTESIAN_POINT('Ctrl Pts',(15.6433901273902,9.69558710884259,-8.65007385040183));
#62395=CARTESIAN_POINT('Ctrl Pts',(15.5613792592266,9.56756393043305,-8.67038126933533));
#62396=CARTESIAN_POINT('Ctrl Pts',(15.4801979882799,9.43901980699784,-8.69077132212474));
#62397=CARTESIAN_POINT('Ctrl Pts',(15.4,9.31004748255804,-8.71122929743643));
#62398=CARTESIAN_POINT('',(15.4,2.88912212849219,-12.4183522790528));
#62399=CARTESIAN_POINT('Origin',(15.4,0.,0.));
#62400=CARTESIAN_POINT('Ctrl Pts',(15.6433901273902,2.64339014463815,-12.7216616660635));
#62401=CARTESIAN_POINT('Ctrl Pts',(15.5613792592266,2.72498847452463,-12.6209440507544));
#62402=CARTESIAN_POINT('Ctrl Pts',(15.4801979882799,2.80691883994236,-12.519816600747));
#62403=CARTESIAN_POINT('Ctrl Pts',(15.4,2.88912212849219,-12.4183522790528));
#62404=CARTESIAN_POINT('Origin',(9.65,-0.756892033916135,20.3476178712976));
#62405=CARTESIAN_POINT('',(9.61650635094611,1.11022302462516E-15,20.8232848254213));
#62406=CARTESIAN_POINT('',(8.50682667397367,-2.21935935394489,20.8232848254213));
#62407=CARTESIAN_POINT('',(9.83301270189222,-2.4,19.1876441793662));
#62408=CARTESIAN_POINT('',(9.53701905283833,-2.69599364905389,19.3585361923259));
#62409=CARTESIAN_POINT('',(9.9,-2.4,19.1102939101766));
#62410=CARTESIAN_POINT('',(12.8327618786655,-2.4,15.7238321899434));
#62411=CARTESIAN_POINT('',(9.9,5.55111512312578E-15,20.4959345562317));
#62412=CARTESIAN_POINT('',(9.9,-0.631892033916135,20.1311115203515));
#62413=CARTESIAN_POINT('',(11.1698262954046,7.21644966006352E-15,19.0296654492799));
#62414=CARTESIAN_POINT('Origin',(0.,-3.46944695195361E-16,20.8232848254213));
#62415=CARTESIAN_POINT('',(9.4,0.433012701892217,20.8232848254213));
#62416=CARTESIAN_POINT('',(6.68182667397366,5.8693593539449,20.8232848254213));
#62417=CARTESIAN_POINT('',(0.,0.433012701892218,20.8232848254213));
#62418=CARTESIAN_POINT('Origin',(7.95,-15.4169872981078,11.9222830587658));
#62419=CARTESIAN_POINT('',(15.3288252219121,-15.4169872981078,11.6722830587658));
#62420=CARTESIAN_POINT('',(7.95,-15.4169872981078,11.6722830587658));
#62421=CARTESIAN_POINT('Ctrl Pts',(15.3288252219121,-15.4169872981078,11.6722830587658));
#62422=CARTESIAN_POINT('Ctrl Pts',(15.2709785585223,-15.4169872981078,11.9203214520311));
#62423=CARTESIAN_POINT('Ctrl Pts',(15.2106539453093,-15.4169872981078,12.1722830587658));
#62424=CARTESIAN_POINT('Origin',(15.15,0.,0.));
#62425=CARTESIAN_POINT('',(15.4,-15.2561953920829,11.5794498085388));
#62426=CARTESIAN_POINT('Ctrl Pts',(15.3288252219121,-15.4169872981078,11.6722830587658));
#62427=CARTESIAN_POINT('Ctrl Pts',(15.36458562618,-15.3362065628442,11.625644279516));
#62428=CARTESIAN_POINT('Ctrl Pts',(15.4,-15.2561953920829,11.5794498085388));
#62429=CARTESIAN_POINT('',(15.9,-13.8109201357914,11.3223700194554));
#62430=CARTESIAN_POINT('Ctrl Pts',(15.9,-13.8109201357914,11.3223700194554));
#62431=CARTESIAN_POINT('Ctrl Pts',(15.6594213742065,-14.5120019863289,11.4493435458609));
#62432=CARTESIAN_POINT('Ctrl Pts',(15.4,-15.2561953920828,11.5794498085388));
#62433=CARTESIAN_POINT('',(15.9,-2.9,17.6217926969611));
#62434=CARTESIAN_POINT('Origin',(15.9,0.,0.));
#62435=CARTESIAN_POINT('',(15.4,-2.4,19.0019776789049));
#62436=CARTESIAN_POINT('Ctrl Pts',(15.4,-2.4,19.0019776789049));
#62437=CARTESIAN_POINT('Ctrl Pts',(15.6594213742039,-2.65942137420393,18.2924341528561));
#62438=CARTESIAN_POINT('Ctrl Pts',(15.9,-2.9,17.6217926969611));
#62439=CARTESIAN_POINT('',(15.3288252219091,-2.4,19.1876441793662));
#62440=CARTESIAN_POINT('Ctrl Pts',(15.4,-2.4,19.0019776789049));
#62441=CARTESIAN_POINT('Ctrl Pts',(15.3645856261785,-2.4,19.094366620863));
#62442=CARTESIAN_POINT('Ctrl Pts',(15.3288252219091,-2.4,19.1876441793662));
#62443=CARTESIAN_POINT('Ctrl Pts',(15.2106539453059,-2.83301270189222,19.4376441793662));
#62444=CARTESIAN_POINT('Ctrl Pts',(15.2709785585168,-2.61480754967826,19.3116633759969));
#62445=CARTESIAN_POINT('Ctrl Pts',(15.3288252219091,-2.4,19.1876441793662));
#62446=CARTESIAN_POINT('Origin',(15.9,-18.7185842870421,13.5784609690827));
#62447=CARTESIAN_POINT('',(9.9,-10.0850287992543,8.59387538414483));
#62448=CARTESIAN_POINT('',(9.9,-8.32627944162883,7.57846096908265));
#62449=CARTESIAN_POINT('',(9.8913964708434,-10.0774525214495,8.58950121811475));
#62450=CARTESIAN_POINT('Ctrl Pts',(9.89139647084313,-10.0774525214493,8.58950121811462));
#62451=CARTESIAN_POINT('Ctrl Pts',(9.89569679092767,-10.0812394300895,8.59168759083744));
#62452=CARTESIAN_POINT('Ctrl Pts',(9.89999999999973,-10.0850287992541,8.59387538414469));
#62453=CARTESIAN_POINT('',(15.4,-10.0774525214495,8.58950121811475));
#62454=CARTESIAN_POINT('',(0.,-10.0774525214495,8.58950121811475));
#62455=CARTESIAN_POINT('',(15.4,-8.75929214352104,7.82846096908265));
#62456=CARTESIAN_POINT('Origin',(9.9,-14.7224318643355,8.5));
#62457=CARTESIAN_POINT('Origin',(9.9,0.,0.));
#62458=CARTESIAN_POINT('Origin',(0.,18.25,10.5366424127107));
#62459=CARTESIAN_POINT('',(9.4,2.83301270189222,19.4376441793662));
#62460=CARTESIAN_POINT('',(9.4,10.0068920339161,15.2958030158883));
#62461=CARTESIAN_POINT('',(15.2106539453093,2.83301270189222,19.4376441793662));
#62462=CARTESIAN_POINT('',(7.95,2.83301270189222,19.4376441793662));
#62463=CARTESIAN_POINT('',(15.2106539453059,15.4169872981078,12.1722830587658));
#62464=CARTESIAN_POINT('Ctrl Pts',(15.2106539453093,2.83301270189222,19.4376441793662));
#62465=CARTESIAN_POINT('Ctrl Pts',(16.2489053918282,9.12499999997897,15.8049636190781));
#62466=CARTESIAN_POINT('Ctrl Pts',(15.2106539453059,15.4169872981078,12.1722830587658));
#62467=CARTESIAN_POINT('',(9.4,15.4169872981078,12.1722830587658));
#62468=CARTESIAN_POINT('',(7.95,15.4169872981078,12.1722830587658));
#62469=CARTESIAN_POINT('',(9.4,17.8169872981078,10.7866424127107));
#62470=CARTESIAN_POINT('',(9.4,17.3681079660839,11.0458030158883));
#62471=CARTESIAN_POINT('',(0.,17.8169872981078,10.7866424127107));
#62472=CARTESIAN_POINT('Origin',(9.65,9.88189203391614,15.0792966649422));
#62473=CARTESIAN_POINT('',(9.9,2.4,19.1102939101766));
#62474=CARTESIAN_POINT('',(9.9,9.75689203391614,14.8627903139961));
#62475=CARTESIAN_POINT('',(9.83301270189222,2.4,19.1876441793662));
#62476=CARTESIAN_POINT('',(11.1671033514046,2.4,17.6471689881276));
#62477=CARTESIAN_POINT('',(8.2334476242669,3.9995650776253,20.1111535075195));
#62478=CARTESIAN_POINT('Origin',(7.95,2.61650635094611,19.3126441793662));
#62479=CARTESIAN_POINT('',(15.3288252219121,2.4,19.1876441793662));
#62480=CARTESIAN_POINT('Ctrl Pts',(15.3288252219121,2.4,19.1876441793662));
#62481=CARTESIAN_POINT('Ctrl Pts',(15.2709785585223,2.6148075496816,19.3116633759989));
#62482=CARTESIAN_POINT('Ctrl Pts',(15.2106539453093,2.83301270189222,19.4376441793662));
#62483=CARTESIAN_POINT('',(7.95,2.4,19.1876441793662));
#62484=CARTESIAN_POINT('Origin',(15.9,2.4,23.));
#62485=CARTESIAN_POINT('',(9.9,2.4,13.0308288301244));
#62486=CARTESIAN_POINT('',(9.9,2.4,11.));
#62487=CARTESIAN_POINT('',(9.89139647084341,2.4,13.0220804980642));
#62488=CARTESIAN_POINT('Ctrl Pts',(9.89139647084313,2.4,13.0220804980639));
#62489=CARTESIAN_POINT('Ctrl Pts',(9.89569679092767,2.4,13.0264532435096));
#62490=CARTESIAN_POINT('Ctrl Pts',(9.89999999999972,2.4,13.0308288301241));
#62491=CARTESIAN_POINT('',(15.4,2.4,13.0220804980642));
#62492=CARTESIAN_POINT('',(0.,2.4,13.0220804980642));
#62493=CARTESIAN_POINT('',(15.4,2.4,19.0019776789123));
#62494=CARTESIAN_POINT('',(15.4,2.4,11.5));
#62495=CARTESIAN_POINT('Ctrl Pts',(15.3288252219121,2.4,19.1876441793662));
#62496=CARTESIAN_POINT('Ctrl Pts',(15.36458562618,2.4,19.0943666208667));
#62497=CARTESIAN_POINT('Ctrl Pts',(15.4,2.4,19.0019776789123));
#62498=CARTESIAN_POINT('Origin',(7.95,-2.61650635094611,19.3126441793662));
#62499=CARTESIAN_POINT('',(7.95,-2.4,19.1876441793662));
#62500=CARTESIAN_POINT('Origin',(15.9,-2.4,11.));
#62501=CARTESIAN_POINT('',(15.4,-2.4,13.0220804980642));
#62502=CARTESIAN_POINT('',(15.4,-2.4,5.5));
#62503=CARTESIAN_POINT('',(9.89139647084341,-2.4,13.0220804980642));
#62504=CARTESIAN_POINT('',(0.,-2.4,13.0220804980642));
#62505=CARTESIAN_POINT('',(9.9,-2.4,13.0308288301244));
#62506=CARTESIAN_POINT('Ctrl Pts',(9.89999999999984,-2.4,13.0308288301242));
#62507=CARTESIAN_POINT('Ctrl Pts',(9.89569679092782,-2.4,13.0264532435097));
#62508=CARTESIAN_POINT('Ctrl Pts',(9.89139647084332,-2.4,13.0220804980641));
#62509=CARTESIAN_POINT('',(9.9,-2.4,23.));
#62510=CARTESIAN_POINT('Origin',(15.65,-2.65,5.5));
#62511=CARTESIAN_POINT('',(15.9,-2.9,12.9287470390599));
#62512=CARTESIAN_POINT('',(15.9,-2.9,5.5));
#62513=CARTESIAN_POINT('',(15.6433901360358,-2.64339013603585,12.7216616766814));
#62514=CARTESIAN_POINT('Ctrl Pts',(15.9,-2.9,12.9287470390599));
#62515=CARTESIAN_POINT('Ctrl Pts',(15.770659214218,-2.77065921421805,12.8252043578707));
#62516=CARTESIAN_POINT('Ctrl Pts',(15.6433901360358,-2.64339013603585,12.7216616766814));
#62517=CARTESIAN_POINT('',(14.6907281821669,-1.6907281821669,13.8975416281819));
#62518=CARTESIAN_POINT('Origin',(15.65,0.,0.));
#62519=CARTESIAN_POINT('',(15.9,-9.74662337492871,8.97584719050482));
#62520=CARTESIAN_POINT('Origin',(15.9,0.,0.));
#62521=CARTESIAN_POINT('',(15.4,-9.31004748255804,8.71122929743642));
#62522=CARTESIAN_POINT('Ctrl Pts',(15.3999999999999,-9.31004748255797,8.71122929743639));
#62523=CARTESIAN_POINT('Ctrl Pts',(15.64392961771,-9.52336184589457,8.84027374524564));
#62524=CARTESIAN_POINT('Ctrl Pts',(15.9,-9.74662337492871,8.97584719050482));
#62525=CARTESIAN_POINT('',(15.4,-2.88912212849219,12.4183522790528));
#62526=CARTESIAN_POINT('Origin',(15.4,0.,0.));
#62527=CARTESIAN_POINT('Ctrl Pts',(15.4,-2.88912212849219,12.4183522790528));
#62528=CARTESIAN_POINT('Ctrl Pts',(15.5187354577638,-2.76741776526553,12.5685731629111));
#62529=CARTESIAN_POINT('Ctrl Pts',(15.6433901360358,-2.64339013603585,12.7216616766814));
#62530=CARTESIAN_POINT('Origin',(15.9,0.,0.));
#62531=CARTESIAN_POINT('',(15.9,-8.50929214352104,8.26147367097487));
#62532=CARTESIAN_POINT('Origin',(15.4,-9.31004748255804,8.71122929743642));
#62533=CARTESIAN_POINT('',(15.4,-9.31004748255804,8.71122929743642));
#62534=CARTESIAN_POINT('',(15.4,-10.0774525214495,8.58950121811475));
#62535=CARTESIAN_POINT('Origin',(15.65,-8.63429214352104,8.04496732002876));
#62536=CARTESIAN_POINT('Origin',(0.,-9.69375000200378,8.65036525777559));
#62537=CARTESIAN_POINT('',(9.4,-9.31004748255804,8.71122929743642));
#62538=CARTESIAN_POINT('',(0.,-9.31004748255804,8.71122929743642));
#62539=CARTESIAN_POINT('Ctrl Pts',(9.8913964708434,-10.0774525214495,8.58950121811475));
#62540=CARTESIAN_POINT('Ctrl Pts',(9.72448837871538,-9.82385455019892,8.62972768575015));
#62541=CARTESIAN_POINT('Ctrl Pts',(9.56028038038363,-9.56780623266559,8.6703428346315));
#62542=CARTESIAN_POINT('Ctrl Pts',(9.4,-9.31004748255804,8.71122929743642));
#62543=CARTESIAN_POINT('Origin',(0.,-12.3383110662499,4.06985113078293));
#62544=CARTESIAN_POINT('',(9.4,-12.1991696110502,3.70712298161641));
#62545=CARTESIAN_POINT('',(0.,-12.1991696110502,3.70712298161641));
#62546=CARTESIAN_POINT('Ctrl Pts',(9.4,-12.1991696110502,3.70712298161641));
#62547=CARTESIAN_POINT('Ctrl Pts',(9.56028038038363,-12.2926402706441,3.95079183865974));
#62548=CARTESIAN_POINT('Ctrl Pts',(9.72448837871538,-12.385490678701,4.19284376068054));
#62549=CARTESIAN_POINT('Ctrl Pts',(9.8913964708434,-12.4774525214495,4.43257927994945));
#62550=CARTESIAN_POINT('Origin',(0.,-12.3383110662499,-4.06985113078293));
#62551=CARTESIAN_POINT('',(9.4,-12.1991696110502,-3.70712298161641));
#62552=CARTESIAN_POINT('Ctrl Pts',(9.8913964708434,-12.4774525214495,-4.43257927994945));
#62553=CARTESIAN_POINT('Ctrl Pts',(9.72448837871531,-12.3854906787009,-4.19284376068043));
#62554=CARTESIAN_POINT('Ctrl Pts',(9.5602803803836,-12.292640270644,-3.95079183865968));
#62555=CARTESIAN_POINT('Ctrl Pts',(9.4,-12.1991696110502,-3.70712298161641));
#62556=CARTESIAN_POINT('',(0.,-12.1991696110502,-3.70712298161641));
#62557=CARTESIAN_POINT('Origin',(0.,-2.6445610642461,-12.7202163885585));
#62558=CARTESIAN_POINT('',(9.89139647084341,-2.4,-13.0220804980642));
#62559=CARTESIAN_POINT('',(0.,-2.4,-13.0220804980642));
#62560=CARTESIAN_POINT('',(9.4,-2.88912212849219,-12.4183522790528));
#62561=CARTESIAN_POINT('Ctrl Pts',(9.89139647084341,-2.4,-13.0220804980642));
#62562=CARTESIAN_POINT('Ctrl Pts',(9.7244883787154,-2.56163612850206,-12.8225714464307));
#62563=CARTESIAN_POINT('Ctrl Pts',(9.56028038038364,-2.72483403797847,-12.6211346732912));
#62564=CARTESIAN_POINT('Ctrl Pts',(9.4,-2.88912212849219,-12.4183522790528));
#62565=CARTESIAN_POINT('',(0.,-2.88912212849219,-12.4183522790528));
#62566=CARTESIAN_POINT('Origin',(0.,2.64456106424609,-12.7202163885585));
#62567=CARTESIAN_POINT('',(9.4,2.88912212849219,-12.4183522790528));
#62568=CARTESIAN_POINT('',(0.,2.88912212849219,-12.4183522790528));
#62569=CARTESIAN_POINT('Ctrl Pts',(9.4,2.88912212849219,-12.4183522790528));
#62570=CARTESIAN_POINT('Ctrl Pts',(9.56028038038363,2.72483403797847,-12.6211346732912));
#62571=CARTESIAN_POINT('Ctrl Pts',(9.72448837871538,2.56163612850207,-12.8225714464307));
#62572=CARTESIAN_POINT('Ctrl Pts',(9.89139647084341,2.4,-13.0220804980642));
#62573=CARTESIAN_POINT('Origin',(0.,9.69375000200378,-8.65036525777559));
#62574=CARTESIAN_POINT('',(9.4,9.31004748255804,-8.71122929743643));
#62575=CARTESIAN_POINT('Ctrl Pts',(9.89139647084341,10.0774525214495,-8.58950121811476));
#62576=CARTESIAN_POINT('Ctrl Pts',(9.72448837871533,9.82385455019883,-8.62972768575017));
#62577=CARTESIAN_POINT('Ctrl Pts',(9.56028038038361,9.56780623266555,-8.67034283463151));
#62578=CARTESIAN_POINT('Ctrl Pts',(9.4,9.31004748255804,-8.71122929743643));
#62579=CARTESIAN_POINT('',(0.,9.31004748255804,-8.71122929743643));
#62580=CARTESIAN_POINT('Origin',(0.,12.3383110662499,-4.06985113078294));
#62581=CARTESIAN_POINT('',(9.89139647084341,12.4774525214495,-4.43257927994946));
#62582=CARTESIAN_POINT('',(15.4,12.4774525214495,-4.43257927994946));
#62583=CARTESIAN_POINT('',(0.,12.4774525214495,-4.43257927994946));
#62584=CARTESIAN_POINT('',(15.6433901361021,12.3389772584149,-4.07158782840527));
#62585=CARTESIAN_POINT('',(14.6907281821669,12.8809881912407,-5.48455725744011));
#62586=CARTESIAN_POINT('',(15.4,12.1991696110502,-3.70712298161642));
#62587=CARTESIAN_POINT('Ctrl Pts',(15.6433901361021,12.3389772584149,-4.07158782840527));
#62588=CARTESIAN_POINT('Ctrl Pts',(15.5187354576438,12.2684125309717,-3.88763249356148));
#62589=CARTESIAN_POINT('Ctrl Pts',(15.3999999996623,12.1991696108533,-3.70712298110308));
#62590=CARTESIAN_POINT('',(9.4,12.1991696110502,-3.70712298161642));
#62591=CARTESIAN_POINT('',(0.,12.1991696110502,-3.70712298161642));
#62592=CARTESIAN_POINT('Ctrl Pts',(9.4,12.1991696110502,-3.70712298161642));
#62593=CARTESIAN_POINT('Ctrl Pts',(9.56028038038363,12.292640270644,-3.95079183865973));
#62594=CARTESIAN_POINT('Ctrl Pts',(9.72448837871537,12.385490678701,-4.19284376068052));
#62595=CARTESIAN_POINT('Ctrl Pts',(9.89139647084341,12.4774525214495,-4.43257927994946));
#62596=CARTESIAN_POINT('Origin',(9.65,0.,0.));
#62597=CARTESIAN_POINT('Ctrl Pts',(9.89999999999984,12.4850287992542,-4.43695344597945));
#62598=CARTESIAN_POINT('Ctrl Pts',(9.89569679092782,12.4812394300896,-4.43476565267222));
#62599=CARTESIAN_POINT('Ctrl Pts',(9.89139647084332,12.4774525214494,-4.43257927994942));
#62600=CARTESIAN_POINT('Origin',(9.4,0.,0.));
#62601=CARTESIAN_POINT('Origin',(9.65,0.,0.));
#62602=CARTESIAN_POINT('',(9.9,-2.4,-13.0308288301244));
#62603=CARTESIAN_POINT('Origin',(9.9,0.,0.));
#62604=CARTESIAN_POINT('Origin',(9.4,0.,0.));
#62605=CARTESIAN_POINT('Ctrl Pts',(9.89139647084313,-2.4,-13.0220804980639));
#62606=CARTESIAN_POINT('Ctrl Pts',(9.89569679092767,-2.4,-13.0264532435096));
#62607=CARTESIAN_POINT('Ctrl Pts',(9.89999999999973,-2.4,-13.0308288301241));
#62608=CARTESIAN_POINT('Origin',(0.,-9.69375000200378,-8.65036525777559));
#62609=CARTESIAN_POINT('',(9.4,-9.31004748255804,-8.71122929743642));
#62610=CARTESIAN_POINT('',(0.,-9.31004748255804,-8.71122929743642));
#62611=CARTESIAN_POINT('',(9.89139647084341,-10.0774525214495,-8.58950121811475));
#62612=CARTESIAN_POINT('Ctrl Pts',(9.4,-9.31004748255804,-8.71122929743642));
#62613=CARTESIAN_POINT('Ctrl Pts',(9.56028038038362,-9.56780623266557,-8.6703428346315));
#62614=CARTESIAN_POINT('Ctrl Pts',(9.72448837871536,-9.82385455019888,-8.62972768575016));
#62615=CARTESIAN_POINT('Ctrl Pts',(9.89139647084341,-10.0774525214495,-8.58950121811475));
#62616=CARTESIAN_POINT('',(0.,-10.0774525214495,-8.58950121811475));
#62617=CARTESIAN_POINT('Origin',(9.65,0.,0.));
#62618=CARTESIAN_POINT('Ctrl Pts',(9.89999999999984,-10.0850287992542,-8.59387538414475));
#62619=CARTESIAN_POINT('Ctrl Pts',(9.89569679092782,-10.0812394300896,-8.59168759083752));
#62620=CARTESIAN_POINT('Ctrl Pts',(9.89139647084332,-10.0774525214494,-8.58950121811471));
#62621=CARTESIAN_POINT('Origin',(9.4,0.,0.));
#62622=CARTESIAN_POINT('Origin',(9.65,0.,0.));
#62623=CARTESIAN_POINT('Origin',(9.4,0.,0.));
#62624=CARTESIAN_POINT('Origin',(0.,-2.64456106424609,12.7202163885585));
#62625=CARTESIAN_POINT('',(9.4,-2.88912212849219,12.4183522790528));
#62626=CARTESIAN_POINT('',(0.,-2.88912212849219,12.4183522790528));
#62627=CARTESIAN_POINT('Ctrl Pts',(9.4,-2.88912212849219,12.4183522790528));
#62628=CARTESIAN_POINT('Ctrl Pts',(9.56028038038363,-2.72483403797847,12.6211346732912));
#62629=CARTESIAN_POINT('Ctrl Pts',(9.72448837871539,-2.56163612850206,12.8225714464307));
#62630=CARTESIAN_POINT('Ctrl Pts',(9.89139647084341,-2.4,13.0220804980642));
#62631=CARTESIAN_POINT('Origin',(0.,0.,0.));
#62632=CARTESIAN_POINT('',(15.4,12.1991696110502,3.70712298161641));
#62633=CARTESIAN_POINT('Origin',(15.4,0.,0.));
#62634=CARTESIAN_POINT('',(9.4,12.1991696110502,3.70712298161641));
#62635=CARTESIAN_POINT('',(0.,12.1991696110502,3.70712298161641));
#62636=CARTESIAN_POINT('',(9.4,9.31004748255805,8.71122929743641));
#62637=CARTESIAN_POINT('Origin',(9.4,0.,0.));
#62638=CARTESIAN_POINT('',(15.4,9.31004748255805,8.71122929743641));
#62639=CARTESIAN_POINT('',(0.,9.31004748255805,8.71122929743641));
#62640=CARTESIAN_POINT('',(15.4,2.88912212849219,12.4183522790528));
#62641=CARTESIAN_POINT('Origin',(15.4,0.,0.));
#62642=CARTESIAN_POINT('',(9.4,2.88912212849219,12.4183522790528));
#62643=CARTESIAN_POINT('',(0.,2.88912212849219,12.4183522790528));
#62644=CARTESIAN_POINT('',(9.4,-1.56142466891288E-15,12.75));
#62645=CARTESIAN_POINT('Origin',(9.4,0.,0.));
#62646=CARTESIAN_POINT('',(0.600000000000001,-1.56142466891288E-15,12.75));
#62647=CARTESIAN_POINT('',(0.,-1.56142466891288E-15,12.75));
#62648=CARTESIAN_POINT('',(0.600000000000003,-12.75,-1.56142466891287E-15));
#62649=CARTESIAN_POINT('Origin',(0.600000000000001,0.,0.));
#62650=CARTESIAN_POINT('Origin',(0.600000000000001,0.,0.));
#62651=CARTESIAN_POINT('Origin',(9.4,0.,0.));
#62652=CARTESIAN_POINT('Origin',(15.65,0.,0.));
#62653=CARTESIAN_POINT('',(15.9,12.6466233749287,-3.95289984855508));
#62654=CARTESIAN_POINT('Ctrl Pts',(15.9,12.6466233749287,-3.95289984855508));
#62655=CARTESIAN_POINT('Ctrl Pts',(15.8143094271252,12.5443697249457,-3.99281062684437));
#62656=CARTESIAN_POINT('Ctrl Pts',(15.7287625868629,12.441814765937,-4.0323814761614));
#62657=CARTESIAN_POINT('Ctrl Pts',(15.6433901361021,12.3389772584547,-4.07158782838998));
#62658=CARTESIAN_POINT('',(15.9,12.6466233749287,3.95289984855507));
#62659=CARTESIAN_POINT('Origin',(15.9,0.,0.));
#62660=CARTESIAN_POINT('Ctrl Pts',(15.4,12.1991696110502,3.7071229816164));
#62661=CARTESIAN_POINT('Ctrl Pts',(15.64392961771,12.4175825627386,3.82733641535336));
#62662=CARTESIAN_POINT('Ctrl Pts',(15.9,12.6466233749287,3.95289984855507));
#62663=CARTESIAN_POINT('Origin',(15.65,6.08813972081441,-0.455032679971241));
#62664=CARTESIAN_POINT('',(15.4,17.6561953920766,-7.42252787036989));
#62665=CARTESIAN_POINT('',(15.4,5.96313972081441,-0.67153903091735));
#62666=CARTESIAN_POINT('',(15.9,16.7109201357914,-6.29942267750569));
#62667=CARTESIAN_POINT('Ctrl Pts',(15.4,17.6561953920766,-7.42252787036989));
#62668=CARTESIAN_POINT('Ctrl Pts',(15.659421374204,17.1714233605295,-6.84309060700007));
#62669=CARTESIAN_POINT('Ctrl Pts',(15.9,16.7109201357914,-6.29942267750569));
#62670=CARTESIAN_POINT('',(15.9,6.21313972081441,-0.238526329025132));
#62671=CARTESIAN_POINT('Origin',(7.95,18.0334936490539,-7.39036112060048));
#62672=CARTESIAN_POINT('',(15.2106539453059,18.25,-7.26536112060048));
#62673=CARTESIAN_POINT('',(7.95,18.25,-7.26536112060048));
#62674=CARTESIAN_POINT('',(15.3288252219092,17.8169872981078,-7.51536112060048));
#62675=CARTESIAN_POINT('Ctrl Pts',(15.2106539453059,18.25,-7.26536112060048));
#62676=CARTESIAN_POINT('Ctrl Pts',(15.2709785585169,18.031794847786,-7.39134192396977));
#62677=CARTESIAN_POINT('Ctrl Pts',(15.3288252219092,17.8169872981078,-7.51536112060048));
#62678=CARTESIAN_POINT('',(7.95,17.8169872981078,-7.51536112060048));
#62679=CARTESIAN_POINT('Origin',(0.,18.0334936490539,-10.4116424127107));
#62680=CARTESIAN_POINT('',(0.,18.25,-10.0366424127107));
#62681=CARTESIAN_POINT('Origin',(15.15,0.,0.));
#62682=CARTESIAN_POINT('',(15.2106539453093,18.25,7.26536112060045));
#62683=CARTESIAN_POINT('Ctrl Pts',(15.2106539453093,18.25,7.26536112060045));
#62684=CARTESIAN_POINT('Ctrl Pts',(16.2489053918282,18.25,2.42850184406507E-11));
#62685=CARTESIAN_POINT('Ctrl Pts',(15.2106539453059,18.25,-7.26536112060048));
#62686=CARTESIAN_POINT('',(15.3288252219121,17.8169872981078,7.51536112060045));
#62687=CARTESIAN_POINT('Ctrl Pts',(15.3288252219121,17.8169872981078,7.51536112060045));
#62688=CARTESIAN_POINT('Ctrl Pts',(15.2709785585222,18.0317948477897,7.39134192396766));
#62689=CARTESIAN_POINT('Ctrl Pts',(15.2106539453093,18.25,7.26536112060045));
#62690=CARTESIAN_POINT('',(15.4,17.6561953920829,7.42252787037345));
#62691=CARTESIAN_POINT('Ctrl Pts',(15.3288252219121,17.8169872981078,7.51536112060045));
#62692=CARTESIAN_POINT('Ctrl Pts',(15.3645856261801,17.736206562844,7.46872234135055));
#62693=CARTESIAN_POINT('Ctrl Pts',(15.4,17.6561953920829,7.42252787037345));
#62694=CARTESIAN_POINT('',(15.9,16.7109201357914,6.29942267750566));
#62695=CARTESIAN_POINT('Ctrl Pts',(15.9,16.7109201357914,6.29942267750567));
#62696=CARTESIAN_POINT('Ctrl Pts',(15.6594213742065,17.1714233605353,6.84309060700057));
#62697=CARTESIAN_POINT('Ctrl Pts',(15.4,17.6561953920829,7.42252787037345));
#62698=CARTESIAN_POINT('Origin',(15.9,0.,0.));
#62699=CARTESIAN_POINT('Ctrl Pts',(15.4,17.6561953920766,-7.42252787036989));
#62700=CARTESIAN_POINT('Ctrl Pts',(15.3645856261794,17.736206562839,-7.46872234134772));
#62701=CARTESIAN_POINT('Ctrl Pts',(15.3288252219092,17.8169872981078,-7.51536112060048));
#62702=CARTESIAN_POINT('Origin',(0.,18.25,-10.5366424127107));
#62703=CARTESIAN_POINT('',(9.4,18.25,10.0366424127107));
#62704=CARTESIAN_POINT('',(0.,18.25,10.0366424127107));
#62705=CARTESIAN_POINT('',(9.4,18.25,7.26536112060045));
#62706=CARTESIAN_POINT('',(9.4,18.25,-1.01832120635535));
#62707=CARTESIAN_POINT('',(7.95,18.25,7.26536112060045));
#62708=CARTESIAN_POINT('Origin',(15.4,2.88912212849219,12.4183522790528));
#62709=CARTESIAN_POINT('',(15.4,2.88912212849219,12.4183522790528));
#62710=CARTESIAN_POINT('',(15.9,2.9,12.9287470390599));
#62711=CARTESIAN_POINT('Ctrl Pts',(15.4,2.88912212849219,12.4183522790528));
#62712=CARTESIAN_POINT('Ctrl Pts',(15.64392961771,2.89422071684404,12.667610160599));
#62713=CARTESIAN_POINT('Ctrl Pts',(15.9,2.9,12.9287470390599));
#62714=CARTESIAN_POINT('',(15.4,2.4,13.0220804980642));
#62715=CARTESIAN_POINT('Origin',(15.4,9.31004748255805,8.71122929743641));
#62716=CARTESIAN_POINT('',(15.9,9.74662337492872,8.97584719050481));
#62717=CARTESIAN_POINT('Ctrl Pts',(15.9,9.74662337492871,8.97584719050482));
#62718=CARTESIAN_POINT('Ctrl Pts',(15.64392961771,9.5233618458946,8.84027374524565));
#62719=CARTESIAN_POINT('Ctrl Pts',(15.4,9.31004748255803,8.71122929743641));
#62720=CARTESIAN_POINT('',(15.4,10.0774525214495,8.58950121811475));
#62721=CARTESIAN_POINT('',(15.4,10.0774525214495,8.58950121811475));
#62722=CARTESIAN_POINT('',(15.9,9.74662337492872,8.97584719050481));
#62723=CARTESIAN_POINT('Origin',(0.,9.69375000200379,8.65036525777558));
#62724=CARTESIAN_POINT('',(9.8913964708434,10.0774525214495,8.58950121811475));
#62725=CARTESIAN_POINT('',(0.,10.0774525214495,8.58950121811475));
#62726=CARTESIAN_POINT('Ctrl Pts',(9.4,9.31004748255805,8.71122929743641));
#62727=CARTESIAN_POINT('Ctrl Pts',(9.56028038038361,9.56780623266555,8.6703428346315));
#62728=CARTESIAN_POINT('Ctrl Pts',(9.72448837871532,9.82385455019883,8.62972768575016));
#62729=CARTESIAN_POINT('Ctrl Pts',(9.8913964708434,10.0774525214495,8.58950121811475));
#62730=CARTESIAN_POINT('Origin',(15.4,12.1991696110502,3.70712298161641));
#62731=CARTESIAN_POINT('',(15.4,12.4774525214495,4.43257927994945));
#62732=CARTESIAN_POINT('',(15.4,12.1991696110502,3.70712298161641));
#62733=CARTESIAN_POINT('',(15.4,12.4774525214495,4.43257927994945));
#62734=CARTESIAN_POINT('Origin',(15.65,11.284292143521,3.45503267997123));
#62735=CARTESIAN_POINT('',(15.4,11.159292143521,3.67153903091734));
#62736=CARTESIAN_POINT('',(15.9,11.409292143521,3.23852632902512));
#62737=CARTESIAN_POINT('Origin',(0.,12.3383110662499,4.06985113078293));
#62738=CARTESIAN_POINT('',(9.89139647084341,12.4774525214495,4.43257927994945));
#62739=CARTESIAN_POINT('',(0.,12.4774525214495,4.43257927994945));
#62740=CARTESIAN_POINT('Ctrl Pts',(9.89139647084341,12.4774525214495,4.43257927994944));
#62741=CARTESIAN_POINT('Ctrl Pts',(9.72448837871538,12.385490678701,4.19284376068052));
#62742=CARTESIAN_POINT('Ctrl Pts',(9.56028038038363,12.2926402706441,3.95079183865972));
#62743=CARTESIAN_POINT('Ctrl Pts',(9.4,12.1991696110502,3.7071229816164));
#62744=CARTESIAN_POINT('Origin',(9.65,0.,0.));
#62745=CARTESIAN_POINT('',(9.9,12.4850287992543,4.43695344597951));
#62746=CARTESIAN_POINT('Ctrl Pts',(9.89139647084313,12.4774525214493,4.4325792799493));
#62747=CARTESIAN_POINT('Ctrl Pts',(9.89569679092767,12.4812394300895,4.43476565267213));
#62748=CARTESIAN_POINT('Ctrl Pts',(9.89999999999972,12.4850287992541,4.43695344597937));
#62749=CARTESIAN_POINT('',(9.9,10.0850287992544,8.59387538414482));
#62750=CARTESIAN_POINT('Origin',(9.9,0.,0.));
#62751=CARTESIAN_POINT('Ctrl Pts',(9.89999999999984,10.0850287992542,8.59387538414474));
#62752=CARTESIAN_POINT('Ctrl Pts',(9.89569679092782,10.0812394300896,8.59168759083751));
#62753=CARTESIAN_POINT('Ctrl Pts',(9.89139647084332,10.0774525214494,8.5895012181147));
#62754=CARTESIAN_POINT('Origin',(15.65,3.43813972081442,5.04496732002876));
#62755=CARTESIAN_POINT('',(15.4,15.2561953920765,11.5794498085351));
#62756=CARTESIAN_POINT('',(15.9,13.8109201357914,11.3223700194554));
#62757=CARTESIAN_POINT('Ctrl Pts',(15.4,15.2561953920765,11.5794498085351));
#62758=CARTESIAN_POINT('Ctrl Pts',(15.6594213742041,14.5120019863252,11.449343545856));
#62759=CARTESIAN_POINT('Ctrl Pts',(15.9,13.8109201357914,11.3223700194554));
#62760=CARTESIAN_POINT('',(15.9,3.31313972081442,5.26147367097487));
#62761=CARTESIAN_POINT('',(15.4,3.56313972081442,4.82846096908265));
#62762=CARTESIAN_POINT('Origin',(15.65,0.,0.));
#62763=CARTESIAN_POINT('Origin',(15.9,0.,0.));
#62764=CARTESIAN_POINT('Origin',(15.65,2.65,11.5));
#62765=CARTESIAN_POINT('',(15.9,2.9,17.6217926969611));
#62766=CARTESIAN_POINT('Ctrl Pts',(15.9,2.9,17.6217926969611));
#62767=CARTESIAN_POINT('Ctrl Pts',(15.6594213742065,2.65942137420647,18.2924341528615));
#62768=CARTESIAN_POINT('Ctrl Pts',(15.4,2.4,19.0019776789123));
#62769=CARTESIAN_POINT('',(15.9,2.9,11.5));
#62770=CARTESIAN_POINT('Origin',(0.,2.64456106424609,12.7202163885585));
#62771=CARTESIAN_POINT('Ctrl Pts',(9.89139647084341,2.4,13.0220804980642));
#62772=CARTESIAN_POINT('Ctrl Pts',(9.72448837871539,2.56163612850206,12.8225714464307));
#62773=CARTESIAN_POINT('Ctrl Pts',(9.56028038038364,2.72483403797846,12.6211346732912));
#62774=CARTESIAN_POINT('Ctrl Pts',(9.4,2.88912212849219,12.4183522790528));
#62775=CARTESIAN_POINT('Origin',(9.65,0.,0.));
#62776=CARTESIAN_POINT('Origin',(9.9,0.,0.));
#62777=CARTESIAN_POINT('Origin',(15.9,10.7262794416288,-3.42153903091735));
#62778=CARTESIAN_POINT('Origin',(9.9,0.,17.));
#62779=CARTESIAN_POINT('Origin',(7.95,15.4169872981078,11.9222830587658));
#62780=CARTESIAN_POINT('',(15.3288252219091,15.4169872981078,11.6722830587658));
#62781=CARTESIAN_POINT('Ctrl Pts',(15.2106539453059,15.4169872981078,12.1722830587658));
#62782=CARTESIAN_POINT('Ctrl Pts',(15.2709785585168,15.4169872981078,11.9203214520272));
#62783=CARTESIAN_POINT('Ctrl Pts',(15.3288252219091,15.4169872981078,11.6722830587658));
#62784=CARTESIAN_POINT('',(9.83301270189222,15.4169872981078,11.6722830587658));
#62785=CARTESIAN_POINT('',(7.95,15.4169872981078,11.6722830587658));
#62786=CARTESIAN_POINT('',(9.83301270189222,15.4169872981078,11.6722830587658));
#62787=CARTESIAN_POINT('Origin',(9.9,17.75,10.2479672781159));
#62788=CARTESIAN_POINT('',(9.4,17.8169872981078,10.7866424127107));
#62789=CARTESIAN_POINT('',(9.9,17.75,10.2479672781159));
#62790=CARTESIAN_POINT('',(9.9,17.75,10.2479672781159));
#62791=CARTESIAN_POINT('',(9.4,18.25,10.0366424127107));
#62792=CARTESIAN_POINT('Origin',(9.65,17.2431079660839,10.8292966649422));
#62793=CARTESIAN_POINT('',(9.9,15.35,11.633607924171));
#62794=CARTESIAN_POINT('',(9.9,17.1181079660839,10.6127903139961));
#62795=CARTESIAN_POINT('',(12.8327618786655,12.4172381213345,9.94037706405436));
#62796=CARTESIAN_POINT('Origin',(7.95,18.0334936490539,7.39036112060045));
#62797=CARTESIAN_POINT('',(9.83301270189222,17.8169872981078,7.51536112060045));
#62798=CARTESIAN_POINT('',(7.95,17.8169872981078,7.51536112060045));
#62799=CARTESIAN_POINT('',(9.4,18.25,7.26536112060045));
#62800=CARTESIAN_POINT('Origin',(9.65,18.,-1.01832120635535));
#62801=CARTESIAN_POINT('',(9.9,17.75,7.47668598600564));
#62802=CARTESIAN_POINT('',(9.9,17.75,-1.01832120635535));
#62803=CARTESIAN_POINT('',(11.1671033514046,16.4828966485954,6.74512352498114));
#62804=CARTESIAN_POINT('Origin',(0.,18.0334936490539,10.4116424127107));
#62805=CARTESIAN_POINT('Origin',(15.15,0.,0.));
#62806=CARTESIAN_POINT('Origin',(15.9,0.,0.));
#62807=CARTESIAN_POINT('Ctrl Pts',(15.4,15.2561953920765,11.5794498085351));
#62808=CARTESIAN_POINT('Ctrl Pts',(15.3645856261785,15.336206562841,11.6256442795142));
#62809=CARTESIAN_POINT('Ctrl Pts',(15.3288252219091,15.4169872981078,11.6722830587658));
#62810=CARTESIAN_POINT('Origin',(0.25,0.,0.));
#62811=CARTESIAN_POINT('',(0.,-13.3071428571429,-1.62965499057966E-15));
#62812=CARTESIAN_POINT('Origin',(0.,0.,0.));
#62813=CARTESIAN_POINT('',(0.25,-13.075,-1.60122568988516E-15));
#62814=CARTESIAN_POINT('Origin',(15.9,21.1185842870421,9.42153903091733));
#62815=CARTESIAN_POINT('',(9.9,10.7262794416288,3.42153903091734));
#62816=CARTESIAN_POINT('Origin',(15.9,8.32627944162883,7.57846096908265));
#62817=CARTESIAN_POINT('',(9.9,18.7185842870421,13.5784609690826));
#62818=CARTESIAN_POINT('Origin',(9.9,14.7224318643355,8.49999999999999));
#62819=CARTESIAN_POINT('Origin',(15.9,0.,0.));
#62820=CARTESIAN_POINT('Origin',(15.9,0.,0.));
#62821=CARTESIAN_POINT('Origin',(15.9,-2.4,-23.));
#62822=CARTESIAN_POINT('',(9.9,-2.4,-11.));
#62823=CARTESIAN_POINT('Origin',(9.9,-2.0818995585505E-15,-17.));
#62824=CARTESIAN_POINT('Origin',(15.9,-8.32627944162883,-7.57846096908265));
#62825=CARTESIAN_POINT('Origin',(0.,-18.25,10.5366424127107));
#62826=CARTESIAN_POINT('Origin',(0.,0.,0.));
#71608=UNCERTAINTY_MEASURE_WITH_UNIT(LENGTH_MEASURE(0.01),#71629,
'DISTANCE_ACCURACY_VALUE',
'Maximum model space distance between geometric entities at asserted c
onnectivities');
#71613=UNCERTAINTY_MEASURE_WITH_UNIT(LENGTH_MEASURE(0.01),#71629,
'DISTANCE_ACCURACY_VALUE',
'Maximum model space distance between geometric entities at asserted c
onnectivities');
#71623=(
GEOMETRIC_REPRESENTATION_CONTEXT(3)
GLOBAL_UNCERTAINTY_ASSIGNED_CONTEXT((#71608))
GLOBAL_UNIT_ASSIGNED_CONTEXT((#71629,#71631,#71632))
REPRESENTATION_CONTEXT('','3D')
);
#71628=(
GEOMETRIC_REPRESENTATION_CONTEXT(3)
GLOBAL_UNCERTAINTY_ASSIGNED_CONTEXT((#71613))
GLOBAL_UNIT_ASSIGNED_CONTEXT((#71629,#71631,#71632))
REPRESENTATION_CONTEXT('','3D')
);
#71629=(
LENGTH_UNIT()
NAMED_UNIT(*)
SI_UNIT(.MILLI.,.METRE.)
);
#71631=(
NAMED_UNIT(*)
PLANE_ANGLE_UNIT()
SI_UNIT($,.RADIAN.)
);
#71632=(
NAMED_UNIT(*)
SI_UNIT($,.STERADIAN.)
SOLID_ANGLE_UNIT()
);
#71642=SHAPE_DEFINITION_REPRESENTATION(#71656,#71691);
#71656=PRODUCT_DEFINITION_SHAPE('',$,#71706);
#71691=SHAPE_REPRESENTATION('',(#37037),#71623);
#71696=PRODUCT_DEFINITION_CONTEXT('part definition',#71740,'design');
#71706=PRODUCT_DEFINITION('2026-10-25-00-23-54-695',
'12_Spindle_Nut_1-14_Slotted',#71720,#71696);
#71720=PRODUCT_DEFINITION_FORMATION('',$,#71751);
#71740=APPLICATION_CONTEXT(
'Core Data for Automotive Mechanical Design Process');
#71741=PRODUCT_CONTEXT('part definition',#71740,'mechanical');
#71751=PRODUCT('2026-10-25-00-23-54-695','12_Spindle_Nut_1-14_Slotted',
$,(#71741));
#71819=COLOUR_RGB('Black',0.12,0.14,0.17);
#71820=FILL_AREA_STYLE_COLOUR('',#71819);
#71821=FILL_AREA_STYLE('',(#71820));
#71822=SURFACE_STYLE_FILL_AREA(#71821);
#71823=SURFACE_SIDE_STYLE('',(#71822));
#71824=SURFACE_STYLE_USAGE(.BOTH.,#71823);
#71825=PRESENTATION_STYLE_ASSIGNMENT((#71824));
ENDSEC;
END-ISO-10303-21;
